ISO-10303-21;
HEADER;
FILE_DESCRIPTION (('STEP AP214'),
    '1' );
FILE_NAME ('Snap Open Cable Crossbars 10.step',
    '2026-10-08T22:59:04',
    ( '' ),
    ( '' ),
    'SwSTEP 2.0',
    'SolidWorks 2020',
    '' );
FILE_SCHEMA (( 'AUTOMOTIVE_DESIGN' ));
ENDSEC;

DATA;
#118=CARTESIAN_POINT ( 'NONE',  ( 22.88900146558018989, 64.28838232313110268, -213.4537907441674918 ) ) ;
#120=ORIENTED_EDGE ( 'NONE', *, *, #167346, .T. ) ;
#437=ORIENTED_EDGE ( 'NONE', *, *, #217472, .F. ) ;
#499=CARTESIAN_POINT ( 'NONE',  ( -16.94132844910802049, 63.05686860792959436, -213.0719227120540609 ) ) ;
#653=CARTESIAN_POINT ( 'NONE',  ( -16.85718274719388177, 60.89144504857533491, -221.1185173850411445 ) ) ;
#743=CARTESIAN_POINT ( 'NONE',  ( -16.80469485234341320, 63.08282825821666506, -213.1683133085603856 ) ) ;
#955=CARTESIAN_POINT ( 'NONE',  ( -16.84793658983402764, 60.96125253478340511, -220.9609974078819903 ) ) ;
#1217=EDGE_LOOP ( 'NONE', ( #94303, #5481, #138383, #26896, #232197 ) ) ;
#1427=LINE ( 'NONE', #80959, #99390 ) ;
#1597=CARTESIAN_POINT ( 'NONE',  ( 12.29592348164039528, 62.46590406472955692, -217.6831045281099932 ) ) ;
#1628=AXIS2_PLACEMENT_3D ( 'NONE', #235147, #253414, #214301 ) ;
#1636=ORIENTED_EDGE ( 'NONE', *, *, #63940, .T. ) ;
#1638=FACE_OUTER_BOUND ( 'NONE', #117688, .T. ) ;
#1858=CARTESIAN_POINT ( 'NONE',  ( -16.97092634996758775, 63.04181532628136608, -213.0951363382118018 ) ) ;
#2005=DIRECTION ( 'NONE',  ( 1.000000000000000000, 0.000000000000000000, 0.000000000000000000 ) ) ;
#2045=CARTESIAN_POINT ( 'NONE',  ( -16.79140778683509438, 63.08531055272182186, -213.1485019413766508 ) ) ;
#2094=CARTESIAN_POINT ( 'NONE',  ( -23.25000000000000355, 60.86901957628278836, -220.9190389461266477 ) ) ;
#2167=DIRECTION ( 'NONE',  ( 1.000000000000000000, 0.000000000000000000, -0.000000000000000000 ) ) ;
#2422=EDGE_CURVE ( 'NONE', #75669, #50778, #138924, .T. ) ;
#2425=AXIS2_PLACEMENT_3D ( 'NONE', #153513, #135160, #16531 ) ;
#2737=EDGE_CURVE ( 'NONE', #240443, #222464, #47177, .T. ) ;
#2745=EDGE_CURVE ( 'NONE', #179633, #22197, #6536, .T. ) ;
#2873=CARTESIAN_POINT ( 'NONE',  ( 14.11444803880198151, 62.02985059084867459, -218.9026721699492839 ) ) ;
#3020=AXIS2_PLACEMENT_3D ( 'NONE', #75505, #59735, #136722 ) ;
#3029=VECTOR ( 'NONE', #222440, 1000.000000000000000 ) ;
#3240=CARTESIAN_POINT ( 'NONE',  ( -18.40000000000000213, 61.64185094745226934, -212.6324159020321076 ) ) ;
#3331=CARTESIAN_POINT ( 'NONE',  ( -16.86422026484316916, 60.90187991312446059, -221.1017989589733759 ) ) ;
#3549=CARTESIAN_POINT ( 'NONE',  ( -16.87683809663752399, 61.23280479334032123, -220.3417702668378126 ) ) ;
#3573=AXIS2_PLACEMENT_3D ( 'NONE', #101158, #99893, #221145 ) ;
#3615=CARTESIAN_POINT ( 'NONE',  ( -18.40000000000000213, 59.60579174656471224, -220.6800530043423976 ) ) ;
#3618=CARTESIAN_POINT ( 'NONE',  ( 20.27550659511088682, 60.75776438711819338, -224.5153016389302536 ) ) ;
#3778=EDGE_LOOP ( 'NONE', ( #190876, #80289, #77411, #221569 ) ) ;
#4166=AXIS2_PLACEMENT_3D ( 'NONE', #98148, #180297, #238993 ) ;
#4205=CARTESIAN_POINT ( 'NONE',  ( 18.54999999999999716, 48.78215419113038109, -213.4964773079645681 ) ) ;
#4621=CARTESIAN_POINT ( 'NONE',  ( -16.87845715379269507, 60.92491586797685699, -221.0649567566318581 ) ) ;
#4657=CARTESIAN_POINT ( 'NONE',  ( -18.39999999999999858, 58.31215475832291162, -223.8520309854405923 ) ) ;
#4739=CARTESIAN_POINT ( 'NONE',  ( 16.27683809663749770, 60.62847850914943137, -224.4802381816402033 ) ) ;
#5015=CARTESIAN_POINT ( 'NONE',  ( -16.94445028196807002, 63.05630424923659660, -213.0754291771441729 ) ) ;
#5034=DIRECTION ( 'NONE',  ( 0.000000000000000000, 0.2617529984165026802, 0.9651348961777159730 ) ) ;
#5174=ORIENTED_EDGE ( 'NONE', *, *, #183969, .F. ) ;
#5362=DIRECTION ( 'NONE',  ( -1.000000000000000000, -1.594516344651357984E-15, 4.324467345337419894E-16 ) ) ;
#5390=CARTESIAN_POINT ( 'NONE',  ( 15.51872946208854565, 62.79551507739390814, -216.3883973845401556 ) ) ;
#5481=ORIENTED_EDGE ( 'NONE', *, *, #83550, .F. ) ;
#5494=EDGE_CURVE ( 'NONE', #39258, #231042, #160972, .T. ) ;
#5601=CARTESIAN_POINT ( 'NONE',  ( -18.40000000000000213, 59.46930106059529919, -220.6430355403071530 ) ) ;
#5808=EDGE_CURVE ( 'NONE', #242911, #151077, #68597, .T. ) ;
#5824=CARTESIAN_POINT ( 'NONE',  ( 20.99999999999999645, 61.13238474529445909, -221.0940783352693586 ) ) ;
#5956=EDGE_LOOP ( 'NONE', ( #13408, #181635, #113316, #249009 ) ) ;
#5980=VERTEX_POINT ( 'NONE', #96357 ) ;
#6012=CARTESIAN_POINT ( 'NONE',  ( -17.01473183483379614, 63.05955705323258798, -213.2241350765465882 ) ) ;
#6101=CARTESIAN_POINT ( 'NONE',  ( -20.65000000000000568, 67.23581240663841641, -214.2531594801197627 ) ) ;
#6151=PLANE ( 'NONE',  #49341 ) ;
#6191=CARTESIAN_POINT ( 'NONE',  ( -13.54036565897075484, 62.93961911720150226, -215.5706779233118482 ) ) ;
#6341=SURFACE_STYLE_USAGE ( .BOTH. , #205841 ) ;
#6536=B_SPLINE_CURVE_WITH_KNOTS ( 'NONE', 3,
 ( #153527, #116913, #215994, #131338, #196439, #111789, #115631, #175620, #235563, #191350 ),
 .UNSPECIFIED., .F., .F.,
 ( 4, 3, 3, 4 ),
 ( 1.903130014847812777E-15, 3.877043166998987006E-05, 7.336897548476661868E-05, 7.659383120239605946E-05 ),
 .UNSPECIFIED. ) ;
#6716=VERTEX_POINT ( 'NONE', #51803 ) ;
#6717=EDGE_CURVE ( 'NONE', #38064, #240443, #198798, .T. ) ;
#6725=CARTESIAN_POINT ( 'NONE',  ( 15.74999999999999645, 62.10905854918434699, -217.1108499610991203 ) ) ;
#7116=DIRECTION ( 'NONE',  ( -1.000000000000000000, 0.000000000000000000, 0.000000000000000000 ) ) ;
#7117=ORIENTED_EDGE ( 'NONE', *, *, #134058, .T. ) ;
#7327=DIRECTION ( 'NONE',  ( 1.000000000000000000, 0.000000000000000000, 0.000000000000000000 ) ) ;
#7570=EDGE_CURVE ( 'NONE', #107985, #209093, #69204, .T. ) ;
#7636=ADVANCED_FACE ( 'NONE', ( #173473 ), #216379, .F. ) ;
#7786=VERTEX_POINT ( 'NONE', #59853 ) ;
#7878=CARTESIAN_POINT ( 'NONE',  ( -13.88555196119804158, 62.02985059084868169, -218.9026721699492555 ) ) ;
#7894=ORIENTED_EDGE ( 'NONE', *, *, #34136, .T. ) ;
#7931=CARTESIAN_POINT ( 'NONE',  ( 15.48841904831874849, 64.42574402712453718, -213.4910444358848167 ) ) ;
#8005=CARTESIAN_POINT ( 'NONE',  ( 13.54577453029514444, 62.93791375105570296, -215.5805554555300887 ) ) ;
#8044=FACE_OUTER_BOUND ( 'NONE', #239798, .T. ) ;
#8138=CARTESIAN_POINT ( 'NONE',  ( 17.23472005113827876, 63.05353557103203599, -211.8790868286480418 ) ) ;
#8774=CARTESIAN_POINT ( 'NONE',  ( -12.25000000000000178, 62.59162599727320497, -217.2417264603073477 ) ) ;
#8866=CARTESIAN_POINT ( 'NONE',  ( -16.79363873026997922, 63.08583527754588260, -213.1316346625713152 ) ) ;
#8869=ORIENTED_EDGE ( 'NONE', *, *, #63940, .F. ) ;
#8899=CARTESIAN_POINT ( 'NONE',  ( -16.81744102076748959, 63.08573235307424198, -213.1276215869287967 ) ) ;
#8925=DIRECTION ( 'NONE',  ( 0.000000000000000000, 0.9993789003877945332, 0.03523937371297191506 ) ) ;
#8929=LINE ( 'NONE', #111892, #59102 ) ;
#9041=ADVANCED_FACE ( 'NONE', ( #131447 ), #29822, .F. ) ;
#9272=CARTESIAN_POINT ( 'NONE',  ( 12.84435279558019438, 62.87834062276079550, -215.9526216959266094 ) ) ;
#9845=PLANE ( 'NONE',  #86860 ) ;
#9933=CIRCLE ( 'NONE', #209864, 0.5000000000000004441 ) ;
#10212=ORIENTED_EDGE ( 'NONE', *, *, #76715, .T. ) ;
#10339=VERTEX_POINT ( 'NONE', #134267 ) ;
#10341=CIRCLE ( 'NONE', #122774, 0.1000000000000124678 ) ;
#10436=CARTESIAN_POINT ( 'NONE',  ( -14.77738660682463134, 62.09660346237241413, -218.7363060264989087 ) ) ;
#10571=CARTESIAN_POINT ( 'NONE',  ( 12.26145404764308644, 62.65055472571233253, -217.0190438104122279 ) ) ;
#10575=DIRECTION ( 'NONE',  ( 0.000000000000000000, 0.2617529984165031243, 0.9651348961777157509 ) ) ;
#10585=ORIENTED_EDGE ( 'NONE', *, *, #93281, .T. ) ;
#10615=LINE ( 'NONE', #190552, #18106 ) ;
#11113=EDGE_CURVE ( 'NONE', #14211, #236891, #191101, .T. ) ;
#11295=ADVANCED_FACE ( 'NONE', ( #155823 ), #16312, .F. ) ;
#11417=CARTESIAN_POINT ( 'NONE',  ( 18.39999999999999503, 61.61567564761062243, -212.7289293916498991 ) ) ;
#11422=DIRECTION ( 'NONE',  ( 0.000000000000000000, -0.9651348961777157509, 0.2617529984165031243 ) ) ;
#11637=CARTESIAN_POINT ( 'NONE',  ( -17.11825945287482753, 60.84284427644114146, -221.0155524357444392 ) ) ;
#11870=CARTESIAN_POINT ( 'NONE',  ( 13.12229106158771685, 62.91120958565417709, -215.7552931531716638 ) ) ;
#12438=DIRECTION ( 'NONE',  ( -1.000000000000000000, 2.670994536826046953E-16, 9.848483305199541222E-16 ) ) ;
#12536=DIRECTION ( 'NONE',  ( 0.000000000000000000, 0.2617529984165031243, 0.9651348961777157509 ) ) ;
#12572=CARTESIAN_POINT ( 'NONE',  ( -18.39999999999999858, 58.59238382117401756, -223.8764022407665379 ) ) ;
#12602=ORIENTED_EDGE ( 'NONE', *, *, #159796, .F. ) ;
#12930=CARTESIAN_POINT ( 'NONE',  ( -17.11825945287482753, 60.96553306590055854, -220.9452142459683159 ) ) ;
#13309=EDGE_CURVE ( 'NONE', #43158, #70322, #51430, .T. ) ;
#13408=ORIENTED_EDGE ( 'NONE', *, *, #183145, .T. ) ;
#13893=AXIS2_PLACEMENT_3D ( 'NONE', #148949, #49826, #44707 ) ;
#14127=VECTOR ( 'NONE', #221090, 1000.000000000000000 ) ;
#14169=CARTESIAN_POINT ( 'NONE',  ( 18.39999999999999503, 61.34848953995435039, -212.6564661897791098 ) ) ;
#14211=VERTEX_POINT ( 'NONE', #14169 ) ;
#14339=EDGE_CURVE ( 'NONE', #158643, #186519, #10341, .T. ) ;
#14357=CARTESIAN_POINT ( 'NONE',  ( 13.99999999999999822, 62.10905854918434699, -217.1108499610991203 ) ) ;
#14568=EDGE_CURVE ( 'NONE', #66070, #136892, #155040, .T. ) ;
#14616=CARTESIAN_POINT ( 'NONE',  ( 22.88900146558018989, 62.14200773611577233, -221.3678968928247457 ) ) ;
#14714=EDGE_CURVE ( 'NONE', #32098, #62912, #143765, .T. ) ;
#15102=ORIENTED_EDGE ( 'NONE', *, *, #160438, .T. ) ;
#15228=CARTESIAN_POINT ( 'NONE',  ( -16.94445028196807002, 63.05630424923659660, -213.0754291771441729 ) ) ;
#15421=CARTESIAN_POINT ( 'NONE',  ( 21.72449340488910252, 60.61704490885460217, -220.9543136786127491 ) ) ;
#15458=FACE_OUTER_BOUND ( 'NONE', #176141, .T. ) ;
#15564=ORIENTED_EDGE ( 'NONE', *, *, #21655, .T. ) ;
#15985=AXIS2_PLACEMENT_3D ( 'NONE', #31478, #53578, #254320 ) ;
#16016=CARTESIAN_POINT ( 'NONE',  ( -16.77431908686106610, 63.08607373851209132, -213.1423865084627209 ) ) ;
#16235=ORIENTED_EDGE ( 'NONE', *, *, #2737, .T. ) ;
#16308=ORIENTED_EDGE ( 'NONE', *, *, #90460, .T. ) ;
#16312=PLANE ( 'NONE',  #72170 ) ;
#16428=ADVANCED_FACE ( 'NONE', ( #200557 ), #156334, .T. ) ;
#16531=DIRECTION ( 'NONE',  ( 1.000000000000000000, 0.000000000000000000, 0.000000000000000000 ) ) ;
#16569=CARTESIAN_POINT ( 'NONE',  ( -18.40000000000000213, 62.49259387941005173, -209.4439336506227960 ) ) ;
#16584=VECTOR ( 'NONE', #232761, 999.9999999999998863 ) ;
#16694=CARTESIAN_POINT ( 'NONE',  ( -17.22361732159832215, 63.03919232351000090, -211.7895729146322026 ) ) ;
#17065=ADVANCED_FACE ( 'NONE', ( #8044 ), #185383, .F. ) ;
#17071=CARTESIAN_POINT ( 'NONE',  ( -16.86420534634261870, 63.08372296379771882, -213.0562714438781313 ) ) ;
#17288=CARTESIAN_POINT ( 'NONE',  ( -16.87683809663752399, 62.98531230502843670, -213.8799296553602005 ) ) ;
#17385=EDGE_CURVE ( 'NONE', #77226, #118476, #56296, .T. ) ;
#17665=DIRECTION ( 'NONE',  ( 1.000000000000000000, -1.145314911736513911E-16, 3.106193895438251633E-17 ) ) ;
#17691=ORIENTED_EDGE ( 'NONE', *, *, #2737, .F. ) ;
#17791=EDGE_CURVE ( 'NONE', #133225, #230526, #157088, .T. ) ;
#18099=DIRECTION ( 'NONE',  ( 1.000000000000000000, 0.000000000000000000, 0.000000000000000000 ) ) ;
#18106=VECTOR ( 'NONE', #108428, 1000.000000000000000 ) ;
#18442=VECTOR ( 'NONE', #79056, 1000.000000000000000 ) ;
#18511=CARTESIAN_POINT ( 'NONE',  ( 20.73486653747088582, 65.69159657275403674, -213.8343546826533554 ) ) ;
#18878=DIRECTION ( 'NONE',  ( 0.000000000000000000, -0.9651348961777157509, 0.2617529984165031243 ) ) ;
#18978=( BOUNDED_SURFACE ( )  B_SPLINE_SURFACE ( 3, 2, ( 
 ( #12930, #233259, #11637 ),
 ( #36332, #155002, #234501 ),
 ( #31226, #170746, #211102 ),
 ( #32506, #112017, #191565 ) ),
 .UNSPECIFIED., .F., .F., .T. ) 
 B_SPLINE_SURFACE_WITH_KNOTS ( ( 4, 4 ),
 ( 3, 3 ),
 ( 4.712388980384689674, 5.765869716888553320 ),
 ( 0.000000000000000000, 1.000000000000000000 ),
 .UNSPECIFIED. ) 
 GEOMETRIC_REPRESENTATION_ITEM ( )  RATIONAL_B_SPLINE_SURFACE ( (
 ( 1.000000000000000000, 0.7071067811865366926, 1.000000000000000000),
 ( 1.000000000000000000, 0.7953136715914939092, 1.000000000000000000),
 ( 1.000000000000000000, 0.8646876308614021012, 1.000000000000000000),
 ( 1.000000000000000000, 0.8984936768950643193, 1.000000000000000000) ) ) 
 REPRESENTATION_ITEM ( '' )  SURFACE ( )  );
#18980=MECHANICAL_DESIGN_GEOMETRIC_PRESENTATION_REPRESENTATION('',(#185591),#93821);
#19038=VERTEX_POINT ( 'NONE', #204538 ) ;
#19101=CARTESIAN_POINT ( 'NONE',  ( -12.25000000000000178, 62.10905854918435409, -217.1108499610990918 ) ) ;
#19167=B_SPLINE_CURVE_WITH_KNOTS ( 'NONE', 3,
 ( #30738, #90667, #33316, #52821, #206781, #148094, #171536, #168982, #129803, #151967, #209336, #227614, #188495, #153259 ),
 .UNSPECIFIED., .F., .F.,
 ( 4, 2, 2, 2, 2, 2, 4 ),
 ( 0.000000000000000000, 2.389617747645413252E-05, 4.779235495290826504E-05, 9.558470990574708694E-05, 0.0001911694198114958273, 0.0003823388396229836857, 0.0007646776792460279783 ),
 .UNSPECIFIED. ) ;
#19276=CARTESIAN_POINT ( 'NONE',  ( -16.93710578446436443, 61.00971801480476842, -220.7822956305894877 ) ) ;
#19313=EDGE_LOOP ( 'NONE', ( #129385, #25235, #108090, #237630 ) ) ;
#19599=ORIENTED_EDGE ( 'NONE', *, *, #57404, .T. ) ;
#19635=CYLINDRICAL_SURFACE ( 'NONE', #95608, 0.1999999999999987899 ) ;
#19772=ORIENTED_EDGE ( 'NONE', *, *, #233839, .T. ) ;
#19857=CARTESIAN_POINT ( 'NONE',  ( -16.84981964351515416, 63.05979328488731284, -213.3481213180943712 ) ) ;
#19992=ORIENTED_EDGE ( 'NONE', *, *, #6717, .F. ) ;
#20213=ORIENTED_EDGE ( 'NONE', *, *, #32150, .T. ) ;
#20234=EDGE_CURVE ( 'NONE', #24894, #87486, #253300, .T. ) ;
#20369=CARTESIAN_POINT ( 'NONE',  ( -16.87372397896795562, 63.02202630553817642, -213.6276555644750204 ) ) ;
#20388=VERTEX_POINT ( 'NONE', #207030 ) ;
#20580=CARTESIAN_POINT ( 'NONE',  ( -16.87998658237717819, 60.99527856349479293, -220.8355367335571771 ) ) ;
#20904=FACE_OUTER_BOUND ( 'NONE', #183304, .T. ) ;
#21056=CARTESIAN_POINT ( 'NONE',  ( -16.81744102076748959, 63.08573235307424198, -213.1276215869287967 ) ) ;
#21270=ORIENTED_EDGE ( 'NONE', *, *, #116453, .T. ) ;
#21312=CYLINDRICAL_SURFACE ( 'NONE', #182406, 0.5000000000000004441 ) ;
#21388=ORIENTED_EDGE ( 'NONE', *, *, #141329, .T. ) ;
#21436=ORIENTED_EDGE ( 'NONE', *, *, #21655, .F. ) ;
#21655=EDGE_CURVE ( 'NONE', #168071, #146129, #147660, .T. ) ;
#21745=CARTESIAN_POINT ( 'NONE',  ( -16.93906926870270624, 60.85410600414655136, -221.1186421532144379 ) ) ;
#21772=CARTESIAN_POINT ( 'NONE',  ( -16.89318236219975944, 63.08559331870877429, -213.1222689416267428 ) ) ;
#21828=VERTEX_POINT ( 'NONE', #118 ) ;
#22006=ORIENTED_EDGE ( 'NONE', *, *, #157312, .T. ) ;
#22140=AXIS2_PLACEMENT_3D ( 'NONE', #240208, #23748, #159388 ) ;
#22197=VERTEX_POINT ( 'NONE', #99355 ) ;
#22211=FACE_OUTER_BOUND ( 'NONE', #158243, .T. ) ;
#22215=DIRECTION ( 'NONE',  ( -1.000000000000000000, 0.000000000000000000, 0.000000000000000000 ) ) ;
#22231=ORIENTED_EDGE ( 'NONE', *, *, #70557, .F. ) ;
#22263=ORIENTED_EDGE ( 'NONE', *, *, #134452, .F. ) ;
#22439=CARTESIAN_POINT ( 'NONE',  ( -18.37160782347004329, 58.57697193133546421, -223.9238517115823299 ) ) ;
#22579=FACE_OUTER_BOUND ( 'NONE', #42947, .T. ) ;
#22933=CARTESIAN_POINT ( 'NONE',  ( 18.39999999999999503, 65.06382255409391746, -210.1412732845728897 ) ) ;
#23151=CARTESIAN_POINT ( 'NONE',  ( -16.89935556175730724, 61.06753202229781152, -220.5691239899323648 ) ) ;
#23333=VECTOR ( 'NONE', #105821, 1000.000000000000000 ) ;
#23338=EDGE_LOOP ( 'NONE', ( #61652, #102377, #66347, #95758 ) ) ;
#23344=ORIENTED_EDGE ( 'NONE', *, *, #98781, .F. ) ;
#23484=LINE ( 'NONE', #63859, #64798 ) ;
#23587=ORIENTED_EDGE ( 'NONE', *, *, #236833, .T. ) ;
#23748=DIRECTION ( 'NONE',  ( 0.000000000000000000, -0.2617529984165031243, -0.9651348961777157509 ) ) ;
#23763=VECTOR ( 'NONE', #237844, 1000.000000000000000 ) ;
#23840=EDGE_LOOP ( 'NONE', ( #16308, #99363 ) ) ;
#24039=CARTESIAN_POINT ( 'NONE',  ( -17.05016517656147101, 63.07979108456520123, -213.1495282149433308 ) ) ;
#24263=DIRECTION ( 'NONE',  ( 0.7071067811865489050, -0.6824534298470359417, 0.1850873201762213704 ) ) ;
#24287=SURFACE_SIDE_STYLE ('',( #124657 ) ) ;
#24437=CARTESIAN_POINT ( 'NONE',  ( -16.80621392010904813, 60.95724664626749956, -221.0055571468712401 ) ) ;
#24604=CARTESIAN_POINT ( 'NONE',  ( -16.77683809663752257, 63.08610022504904435, -213.1421742787362064 ) ) ;
#24661=FACE_BOUND ( 'NONE', #176978, .T. ) ;
#24894=VERTEX_POINT ( 'NONE', #88244 ) ;
#25058=LINE ( 'NONE', #168448, #23333 ) ;
#25235=ORIENTED_EDGE ( 'NONE', *, *, #161274, .T. ) ;
#25315=ADVANCED_FACE ( 'NONE', ( #192220 ), #172692, .T. ) ;
#25348=ADVANCED_FACE ( 'NONE', ( #83056 ), #65456, .F. ) ;
#25424=CARTESIAN_POINT ( 'NONE',  ( -16.84421487269768392, 60.94446250508437402, -221.0229055566649663 ) ) ;
#25538=DIRECTION ( 'NONE',  ( -1.020425574104004196E-15, 0.2617529984165031243, 0.9651348961777157509 ) ) ;
#25561=( NAMED_UNIT ( * ) SI_UNIT ( $, .STERADIAN. ) SOLID_ANGLE_UNIT ( ) );
#25619=LINE ( 'NONE', #122151, #163205 ) ;
#25621=DIRECTION ( 'NONE',  ( -0.7071067811865489050, -0.6824534298470359417, 0.1850873201762213704 ) ) ;
#25669=DIRECTION ( 'NONE',  ( -3.035766082959430717E-14, 0.2617529984165031243, 0.9651348961777157509 ) ) ;
#25766=CARTESIAN_POINT ( 'NONE',  ( -12.92414019175886253, 62.89253001998297776, -215.8738493471900028 ) ) ;
#25976=VERTEX_POINT ( 'NONE', #94221 ) ;
#26153=CARTESIAN_POINT ( 'NONE',  ( -14.45443560709636621, 62.05118075326794980, -218.8501529344108008 ) ) ;
#26405=VECTOR ( 'NONE', #59370, 1000.000000000000000 ) ;
#26432=LINE ( 'NONE', #48542, #207344 ) ;
#26436=CARTESIAN_POINT ( 'NONE',  ( 18.39999999999997371, 58.31215475832291162, -223.8520309854405923 ) ) ;
#26508=EDGE_CURVE ( 'NONE', #222464, #155345, #120347, .T. ) ;
#26639=ORIENTED_EDGE ( 'NONE', *, *, #47376, .T. ) ;
#26896=ORIENTED_EDGE ( 'NONE', *, *, #152057, .F. ) ;
#27011=DIRECTION ( 'NONE',  ( -1.020425574104004196E-15, 0.2617529984165031243, 0.9651348961777157509 ) ) ;
#27024=B_SPLINE_CURVE_WITH_KNOTS ( 'NONE', 3,
 ( #141577, #162449, #103709, #205386, #3331, #161156, #221104, #4621, #241958, #63314 ),
 .UNSPECIFIED., .F., .F.,
 ( 4, 3, 3, 4 ),
 ( 0.000000000000000000, 4.874959354402766518E-05, 9.785140065120894143E-05, 0.0001360444631936018149 ),
 .UNSPECIFIED. ) ;
#27084=CARTESIAN_POINT ( 'NONE',  ( -14.87770893841227249, 62.91120958565418420, -215.7552931531716354 ) ) ;
#27216=VERTEX_POINT ( 'NONE', #6725 ) ;
#27237=DIRECTION ( 'NONE',  ( 0.2834754621636358940, 0.03379383663320500997, -0.9583838682682015442 ) ) ;
#27460=ORIENTED_EDGE ( 'NONE', *, *, #135985, .T. ) ;
#27596=ORIENTED_EDGE ( 'NONE', *, *, #248128, .F. ) ;
#27842=AXIS2_PLACEMENT_3D ( 'NONE', #104937, #241909, #2005 ) ;
#27957=ADVANCED_FACE ( 'NONE', ( #246955 ), #189575, .F. ) ;
#28008=CARTESIAN_POINT ( 'NONE',  ( -16.86132326855788577, 60.95208832852619452, -220.9947876425996753 ) ) ;
#28230=EDGE_CURVE ( 'NONE', #38064, #238512, #240255, .T. ) ;
#28469=CARTESIAN_POINT ( 'NONE',  ( -16.77779411440718249, 63.08607716446275049, -213.1412442136428922 ) ) ;
#28619=DIRECTION ( 'NONE',  ( 1.000000000000000000, 0.000000000000000000, 0.000000000000000000 ) ) ;
#28943=B_SPLINE_CURVE_WITH_KNOTS ( 'NONE', 3,
 ( #163451, #203849, #179188, #83862, #242974, #223402, #60475, #142578, #64354, #198715, #61776, #143869, #222105, #200011, #499, #80018 ),
 .UNSPECIFIED., .F., .F.,
 ( 4, 3, 3, 3, 3, 4 ),
 ( 0.000000000000000000, 1.810570668010542492E-05, 2.740575833570115904E-05, 4.256816319434871692E-05, 5.213463471023795320E-05, 6.641585710717593048E-05 ),
 .UNSPECIFIED. ) ;
#29066=LINE ( 'NONE', #108565, #72586 ) ;
#29311=VECTOR ( 'NONE', #223988, 1000.000000000000000 ) ;
#29379=CARTESIAN_POINT ( 'NONE',  ( -17.78241384943553172, 59.43689591760609403, -223.1219430936941990 ) ) ;
#29651=CARTESIAN_POINT ( 'NONE',  ( -15.06720934482788010, 62.89055100415842503, -215.8809258249639242 ) ) ;
#29730=ORIENTED_EDGE ( 'NONE', *, *, #14339, .F. ) ;
#29822=PLANE ( 'NONE',  #70468 ) ;
#30019=CARTESIAN_POINT ( 'NONE',  ( -12.60206096961792177, 62.27137470634865934, -218.2709398499965801 ) ) ;
#30188=ORIENTED_EDGE ( 'NONE', *, *, #74783, .T. ) ;
#30322=ORIENTED_EDGE ( 'NONE', *, *, #248128, .T. ) ;
#30617=DIRECTION ( 'NONE',  ( 0.7071067811865546782, -0.6824534298470523730, 0.1850873201761376874 ) ) ;
#30738=CARTESIAN_POINT ( 'NONE',  ( -16.77683809663752257, 60.94702803318471496, -221.0293550571836647 ) ) ;
#30754=EDGE_CURVE ( 'NONE', #102030, #124122, #127011, .T. ) ;
#30857=CARTESIAN_POINT ( 'NONE',  ( -18.39999999999999858, 58.59921997668411819, -223.8511959880075608 ) ) ;
#31226=CARTESIAN_POINT ( 'NONE',  ( -16.92209698673438822, 60.95522930754523117, -220.9832062338754781 ) ) ;
#31241=CARTESIAN_POINT ( 'NONE',  ( -23.25000000000000355, 58.31215475832291162, -223.8520309854405923 ) ) ;
#31312=CARTESIAN_POINT ( 'NONE',  ( -14.23072895065542909, 62.03428458984607374, -218.8918409208595222 ) ) ;
#31353=EDGE_CURVE ( 'NONE', #77226, #32098, #100347, .T. ) ;
#31440=CARTESIAN_POINT ( 'NONE',  ( -20.65000000000000568, 65.69159657275406516, -213.8343546826533839 ) ) ;
#31477=VERTEX_POINT ( 'NONE', #209751 ) ;
#31478=CARTESIAN_POINT ( 'NONE',  ( 13.99999999999999822, 62.10905854918434699, -217.1108499610991203 ) ) ;
#31557=VECTOR ( 'NONE', #57339, 1000.000000000000114 ) ;
#31755=CARTESIAN_POINT ( 'NONE',  ( -15.75000000000000000, 62.53182050776837286, -217.4622410876595779 ) ) ;
#32030=CIRCLE ( 'NONE', #165272, 0.09999999999999371891 ) ;
#32098=VERTEX_POINT ( 'NONE', #125436 ) ;
#32150=EDGE_CURVE ( 'NONE', #115941, #198538, #241520, .T. ) ;
#32495=EDGE_CURVE ( 'NONE', #209093, #238512, #23484, .T. ) ;
#32506=CARTESIAN_POINT ( 'NONE',  ( -16.87242674293849731, 60.93907239080193250, -221.0427799704054621 ) ) ;
#32665=DIRECTION ( 'NONE',  ( 0.7071067811865463515, -0.6824534298470387172, 0.1850873201762205933 ) ) ;
#32737=FACE_OUTER_BOUND ( 'NONE', #97242, .T. ) ;
#33001=ORIENTED_EDGE ( 'NONE', *, *, #173115, .F. ) ;
#33120=AXIS2_PLACEMENT_3D ( 'NONE', #196308, #17665, #179346 ) ;
#33141=EDGE_CURVE ( 'NONE', #229612, #67123, #215867, .T. ) ;
#33220=ADVANCED_FACE ( 'NONE', ( #137614 ), #221010, .F. ) ;
#33245=EDGE_CURVE ( 'NONE', #137276, #116061, #200261, .T. ) ;
#33316=CARTESIAN_POINT ( 'NONE',  ( -16.79139129368507355, 60.94953642464052734, -221.0235123146207172 ) ) ;
#33484=EDGE_LOOP ( 'NONE', ( #33001, #44586, #110798, #206880 ) ) ;
#33700=CARTESIAN_POINT ( 'NONE',  ( 20.73486653747088937, 65.20902912466516455, -213.7034781834451280 ) ) ;
#34136=EDGE_CURVE ( 'NONE', #180612, #230787, #68725, .T. ) ;
#34200=VECTOR ( 'NONE', #131142, 1000.000000000000000 ) ;
#34217=DIRECTION ( 'NONE',  ( 1.020425574104004196E-15, -0.2617529984165031243, -0.9651348961777157509 ) ) ;
#34917=ADVANCED_FACE ( 'NONE', ( #170180 ), #226916, .T. ) ;
#35149=CARTESIAN_POINT ( 'NONE',  ( 20.05000000000002913, 65.69159657275403674, -213.8343546826533554 ) ) ;
#35203=CARTESIAN_POINT ( 'NONE',  ( -16.81744102076749314, 60.93935776605891164, -221.0417277355860790 ) ) ;
#35204=VECTOR ( 'NONE', #229270, 1000.000000000000000 ) ;
#35287=ORIENTED_EDGE ( 'NONE', *, *, #241584, .T. ) ;
#35410=CARTESIAN_POINT ( 'NONE',  ( -17.11825945287482753, 60.96553306590055854, -220.9452142459683159 ) ) ;
#35496=B_SPLINE_CURVE_WITH_KNOTS ( 'NONE', 3,
 ( #24604, #207070, #28469, #107964, #83232, #162822, #8866, #88370, #167970, #51813 ),
 .UNSPECIFIED., .F., .F.,
 ( 4, 3, 3, 4 ),
 ( -2.000561356221172119E-06, 0.000000000000000000, 1.787822682429087714E-05, 4.206475347090508942E-05 ),
 .UNSPECIFIED. ) ;
#35583=CARTESIAN_POINT ( 'NONE',  ( -16.87998658237703964, 63.02981155563863069, -213.3338125889567038 ) ) ;
#35671=AXIS2_PLACEMENT_3D ( 'NONE', #4205, #47169, #244102 ) ;
#35781=EDGE_CURVE ( 'NONE', #110195, #151077, #119505, .T. ) ;
#35818=CARTESIAN_POINT ( 'NONE',  ( -21.65000000000000213, 63.54522198573874192, -221.7484608313106378 ) ) ;
#36003=ADVANCED_FACE ( 'NONE', ( #223707 ), #245860, .T. ) ;
#36086=VERTEX_POINT ( 'NONE', #35818 ) ;
#36332=CARTESIAN_POINT ( 'NONE',  ( -17.01764560440540919, 60.96553306569528274, -220.9452142467251576 ) ) ;
#36414=PLANE ( 'NONE',  #50419 ) ;
#36829=ORIENTED_EDGE ( 'NONE', *, *, #32150, .F. ) ;
#36969=CARTESIAN_POINT ( 'NONE',  ( 21.13736287352038445, 64.92272921553191622, -213.6258311519692086 ) ) ;
#36976=PLANE ( 'NONE',  #1628 ) ;
#37187=CARTESIAN_POINT ( 'NONE',  ( -18.40000000000000213, 65.08943781962308606, -222.1672656287770451 ) ) ;
#37290=( BOUNDED_SURFACE ( )  B_SPLINE_SURFACE ( 3, 2, ( 
 ( #118062, #254942, #115490 ),
 ( #161056, #80184, #653 ),
 ( #136311, #159771, #236710 ),
 ( #58066, #120660, #155937 ) ),
 .UNSPECIFIED., .F., .F., .T. ) 
 B_SPLINE_SURFACE_WITH_KNOTS ( ( 4, 4 ),
 ( 3, 3 ),
 ( 0.0008258556059633741101, 0.0009616864997632722234 ),
 ( 0.000000000000000000, 1.000000000000000000 ),
 .UNSPECIFIED. ) 
 GEOMETRIC_REPRESENTATION_ITEM ( )  RATIONAL_B_SPLINE_SURFACE ( (
 ( 1.000000000000000000, 0.9152888060719065466, 1.000000000000000000),
 ( 1.000000000000000000, 0.9327727094138433817, 1.000000000000000000),
 ( 1.000000000000000000, 0.9369023509258295190, 1.000000000000000000),
 ( 1.000000000000000000, 0.9246339933864298199, 1.000000000000000000) ) ) 
 REPRESENTATION_ITEM ( '' )  SURFACE ( )  );
#37348=EDGE_CURVE ( 'NONE', #107985, #62912, #98336, .T. ) ;
#37359=DIRECTION ( 'NONE',  ( -0.000000000000000000, 0.2617529984165031243, 0.9651348961777157509 ) ) ;
#37383=AXIS2_PLACEMENT_3D ( 'NONE', #246324, #67680, #147218 ) ;
#37399=EDGE_LOOP ( 'NONE', ( #247895, #132383, #41039, #30188 ) ) ;
#37428=VECTOR ( 'NONE', #139047, 1000.000000000000000 ) ;
#37539=APPLICATION_CONTEXT ( 'automotive_design' ) ;
#37571=DIRECTION ( 'NONE',  ( 0.000000000000000000, -0.2617529984165152257, -0.9651348961777124202 ) ) ;
#37753=CARTESIAN_POINT ( 'NONE',  ( -16.79814274880124358, 60.94069671524907505, -221.0395699407627887 ) ) ;
#37775=DIRECTION ( 'NONE',  ( -1.000000000000000000, 0.000000000000000000, 0.000000000000000000 ) ) ;
#37799=AXIS2_PLACEMENT_3D ( 'NONE', #75110, #191205, #52938 ) ;
#38064=VERTEX_POINT ( 'NONE', #242258 ) ;
#38079=DIRECTION ( 'NONE',  ( 1.186688945009010077E-16, 0.9651348961777157509, -0.2617529984165031243 ) ) ;
#38138=CARTESIAN_POINT ( 'NONE',  ( -16.79270642812317504, 63.08646044285087839, -213.1392855534523676 ) ) ;
#38145=CIRCLE ( 'NONE', #254575, 0.9000000000000014655 ) ;
#38188=CARTESIAN_POINT ( 'NONE',  ( 13.12220780326573788, 62.11640146696787923, -218.6859212199908029 ) ) ;
#38198=DIRECTION ( 'NONE',  ( -1.020425574104004196E-15, -0.2617529984165031243, -0.9651348961777157509 ) ) ;
#38367=CARTESIAN_POINT ( 'NONE',  ( -17.01825945287481545, 63.05955705323258798, -213.2241350765465882 ) ) ;
#38449=LINE ( 'NONE', #37187, #116833 ) ;
#38622=DIRECTION ( 'NONE',  ( 0.000000000000000000, 0.9651348961777157509, -0.2617529984165031243 ) ) ;
#38929=ORIENTED_EDGE ( 'NONE', *, *, #185988, .F. ) ;
#39258=VERTEX_POINT ( 'NONE', #31440 ) ;
#39377=PLANE ( 'NONE',  #212502 ) ;
#39438=CARTESIAN_POINT ( 'NONE',  ( -16.83233564386394931, 63.07197639479962703, -213.2539030774048570 ) ) ;
#39541=LINE ( 'NONE', #40821, #143688 ) ;
#39598=CARTESIAN_POINT ( 'NONE',  ( 20.73486653747088937, 62.17269434303373288, -224.8990429791066106 ) ) ;
#39653=LINE ( 'NONE', #257322, #94390 ) ;
#39699=ORIENTED_EDGE ( 'NONE', *, *, #30754, .F. ) ;
#39830=VERTEX_POINT ( 'NONE', #181838 ) ;
#39849=DIRECTION ( 'NONE',  ( -1.073024830501117725E-15, -0.2617529984165031243, -0.9651348961777157509 ) ) ;
#39915=LINE ( 'NONE', #99820, #171483 ) ;
#40013=( NAMED_UNIT ( * ) PLANE_ANGLE_UNIT ( ) SI_UNIT ( $, .RADIAN. ) );
#40156=CARTESIAN_POINT ( 'NONE',  ( -16.92280123533700120, 60.99187387584997566, -220.8480904879614855 ) ) ;
#40293=CARTESIAN_POINT ( 'NONE',  ( -16.87435696428308063, 60.93935323350471833, -221.0417350386312876 ) ) ;
#40383=ADVANCED_FACE ( 'NONE', ( #71873 ), #152711, .F. ) ;
#40425=VECTOR ( 'NONE', #159079, 1000.000000000000000 ) ;
#40726=CARTESIAN_POINT ( 'NONE',  ( -16.83558968593875349, 63.08251143331946054, -213.1394977529018036 ) ) ;
#40821=CARTESIAN_POINT ( 'NONE',  ( 18.39999999999999503, 62.23844973457045882, -209.3750075427748527 ) ) ;
#40999=CARTESIAN_POINT ( 'NONE',  ( -17.78241384945978965, 62.84018868124818624, -210.5733318916599046 ) ) ;
#41039=ORIENTED_EDGE ( 'NONE', *, *, #14714, .T. ) ;
#41134=AXIS2_PLACEMENT_3D ( 'NONE', #164067, #109201, #208342 ) ;
#41235=B_SPLINE_CURVE_WITH_KNOTS ( 'NONE', 3,
 ( #156824, #79792, #22439, #96779, #219320, #138478, #81082 ),
 .UNSPECIFIED., .F., .F.,
 ( 4, 3, 4 ),
 ( 0.000000000000000000, 4.520325912680747552E-05, 5.794988040901532806E-05 ),
 .UNSPECIFIED. ) ;
#41323=CARTESIAN_POINT ( 'NONE',  ( -16.93440969289731157, 60.88036584781310978, -221.0866173190812276 ) ) ;
#41332=ADVANCED_FACE ( 'NONE', ( #175494 ), #141222, .T. ) ;
#41348=ADVANCED_FACE ( 'NONE', ( #256216 ), #37290, .T. ) ;
#41350=CARTESIAN_POINT ( 'NONE',  ( -16.89797118371611973, 63.08312069776565068, -213.0364664784391664 ) ) ;
#41385=VECTOR ( 'NONE', #179989, 1000.000000000000000 ) ;
#41428=CARTESIAN_POINT ( 'NONE',  ( -16.83233564386401326, 60.99129099293333667, -220.9258002532045566 ) ) ;
#41655=CARTESIAN_POINT ( 'NONE',  ( -21.64999999999999858, 63.66481329078087015, -213.2846733859786923 ) ) ;
#41666=ADVANCED_FACE ( 'NONE', ( #22211 ), #19635, .T. ) ;
#41772=LINE ( 'NONE', #200828, #41385 ) ;
#41786=CARTESIAN_POINT ( 'NONE',  ( 20.73486653747088937, 63.06265453764984841, -221.6175843321023819 ) ) ;
#41894=ADVANCED_FACE ( 'NONE', ( #74198 ), #18978, .T. ) ;
#42040=CARTESIAN_POINT ( 'NONE',  ( 13.76927104934458335, 62.03428458984606664, -218.8918409208596074 ) ) ;
#42299=CARTESIAN_POINT ( 'NONE',  ( -16.87242674293849731, 63.08601772833120691, -213.1265693521094136 ) ) ;
#42407=DIRECTION ( 'NONE',  ( 1.000000000000000000, 0.000000000000000000, 0.000000000000000000 ) ) ;
#42467=LINE ( 'NONE', #201540, #94292 ) ;
#42683=EDGE_LOOP ( 'NONE', ( #76966, #19772, #7894, #96060, #195626, #106918, #113762, #132799, #44666 ) ) ;
#42687=CARTESIAN_POINT ( 'NONE',  ( -16.87683809663750267, 61.13629130372253684, -220.3155949669961160 ) ) ;
#42741=VECTOR ( 'NONE', #153272, 1000.000000000000000 ) ;
#42849=CYLINDRICAL_SURFACE ( 'NONE', #108072, 1.749999999999999778 ) ;
#42947=EDGE_LOOP ( 'NONE', ( #38929, #124642, #15564, #178574 ) ) ;
#43086=DIRECTION ( 'NONE',  ( 1.000000000000000000, 0.000000000000000000, 0.000000000000000000 ) ) ;
#43158=VERTEX_POINT ( 'NONE', #116966 ) ;
#43284=PLANE ( 'NONE',  #22140 ) ;
#43585=FACE_OUTER_BOUND ( 'NONE', #237500, .T. ) ;
#43970=CARTESIAN_POINT ( 'NONE',  ( -16.85697194749148764, 61.05396939583364002, -220.7775114784828361 ) ) ;
#43997=APPLICATION_CONTEXT ( 'automotive_design' ) ;
#44049=CARTESIAN_POINT ( 'NONE',  ( -15.31895204843006120, 62.84928511903725479, -216.1139082291015256 ) ) ;
#44091=ORIENTED_EDGE ( 'NONE', *, *, #11113, .T. ) ;
#44108=CARTESIAN_POINT ( 'NONE',  ( -16.87487986503753845, 60.93934386241939904, -221.0417501376295775 ) ) ;
#44344=VECTOR ( 'NONE', #42407, 1000.000000000000000 ) ;
#44586=ORIENTED_EDGE ( 'NONE', *, *, #57388, .F. ) ;
#44666=ORIENTED_EDGE ( 'NONE', *, *, #139703, .F. ) ;
#44707=DIRECTION ( 'NONE',  ( -1.000000000000000000, 0.000000000000000000, 0.000000000000000000 ) ) ;
#44898=AXIS2_PLACEMENT_3D ( 'NONE', #239509, #156144, #99957 ) ;
#45150=CARTESIAN_POINT ( 'NONE',  ( -17.11825945287481332, 63.05955705323258798, -213.2241350765465882 ) ) ;
#45300=FACE_OUTER_BOUND ( 'NONE', #246696, .T. ) ;
#45327=CARTESIAN_POINT ( 'NONE',  ( -14.77538296656415362, 62.91973165888632735, -215.7008495347502617 ) ) ;
#45459=DIRECTION ( 'NONE',  ( -1.020425574104004196E-15, 0.2617529984165031243, 0.9651348961777157509 ) ) ;
#45554=ORIENTED_EDGE ( 'NONE', *, *, #135235, .F. ) ;
#45626=FACE_OUTER_BOUND ( 'NONE', #229785, .T. ) ;
#45723=CARTESIAN_POINT ( 'NONE',  ( -16.87331047859651179, 60.93935776605891164, -221.0417277355860790 ) ) ;
#45761=CARTESIAN_POINT ( 'NONE',  ( -18.40000000000000213, 59.60579174656471224, -220.6800530043423976 ) ) ;
#45816=EDGE_CURVE ( 'NONE', #50778, #70322, #151242, .T. ) ;
#45872=DIRECTION ( 'NONE',  ( -1.646408749285563007E-14, -0.9651348961777157509, 0.2617529984165031243 ) ) ;
#45955=ORIENTED_EDGE ( 'NONE', *, *, #51871, .F. ) ;
#46303=EDGE_CURVE ( 'NONE', #146129, #83517, #9933, .T. ) ;
#46398=CARTESIAN_POINT ( 'NONE',  ( -20.65000000000000568, 62.65526179112262639, -225.0299194783148948 ) ) ;
#46444=DIRECTION ( 'NONE',  ( 0.000000000000000000, -0.2617529984165031243, -0.9651348961777157509 ) ) ;
#47092=CARTESIAN_POINT ( 'NONE',  ( 14.88075390448863722, 62.91308081279556319, -215.7443727990306002 ) ) ;
#47117=B_SPLINE_CURVE_WITH_KNOTS ( 'NONE', 3,
 ( #8774, #85695, #88272, #68752, #146975, #208270, #105258, #248663, #244801, #25766, #226505, #6191, #148282, #47880, #227807, #124871, #49175, #45327, #27084, #29651, #109137, #44049, #184828, #169162, #123586, #66175, #145697, #164002, #106562, #203114 ),
 .UNSPECIFIED., .F., .F.,
 ( 4, 2, 2, 2, 2, 2, 2, 2, 2, 2, 2, 2, 2, 2, 4 ),
 ( 0.000000000000000000, 0.0003422764154113331811, 0.0006845528308226663623, 0.001026829246233999489, 0.001369105661645332725, 0.002053658492468004183, 0.002738211323290676291, 0.003080487738702012129, 0.003422764154113347532, 0.003765040569524683370, 0.004107316984936018774, 0.004449593400347354177, 0.004791869815758689581, 0.005134146231170025852, 0.005476422646581361256 ),
 .UNSPECIFIED. ) ;
#47169=DIRECTION ( 'NONE',  ( 1.000000000000000000, 0.000000000000000000, 0.000000000000000000 ) ) ;
#47177=B_SPLINE_CURVE_WITH_KNOTS ( 'NONE', 3,
 ( #255080, #174371, #251276, #71392 ),
 .UNSPECIFIED., .F., .F.,
 ( 4, 4 ),
 ( 0.000000000000000000, 7.713889350927705709E-05 ),
 .UNSPECIFIED. ) ;
#47376=EDGE_CURVE ( 'NONE', #51883, #90818, #10615, .T. ) ;
#47595=CARTESIAN_POINT ( 'NONE',  ( -16.87036670365549540, 60.86740053880574663, -221.1564527318009539 ) ) ;
#47634=VECTOR ( 'NONE', #201734, 1000.000000000000000 ) ;
#47668=CARTESIAN_POINT ( 'NONE',  ( 18.39999999999999503, 65.08943781962308606, -222.1672656287770451 ) ) ;
#47880=CARTESIAN_POINT ( 'NONE',  ( -14.11361717019516071, 62.94602368561173478, -215.5245807872942976 ) ) ;
#47947=CARTESIAN_POINT ( 'NONE',  ( -16.89268316805466341, 60.93619025550653134, -221.0468289635910537 ) ) ;
#48267=CARTESIAN_POINT ( 'NONE',  ( -12.29659703204452370, 62.46518123923912214, -217.6854569796042540 ) ) ;
#48487=EDGE_CURVE ( 'NONE', #5980, #66070, #177437, .T. ) ;
#48542=CARTESIAN_POINT ( 'NONE',  ( -18.40000000000000213, 62.50563584222672375, -209.4474707446456421 ) ) ;
#49138=CARTESIAN_POINT ( 'NONE',  ( -16.27683809663750480, 60.62847850914943137, -224.4802381816402317 ) ) ;
#49175=CARTESIAN_POINT ( 'NONE',  ( -14.56336952470180179, 62.93307127222839625, -215.6135269849708607 ) ) ;
#49308=EDGE_LOOP ( 'NONE', ( #238676, #131710, #141585, #83052, #229085, #27460 ) ) ;
#49341=AXIS2_PLACEMENT_3D ( 'NONE', #49138, #128697, #208240 ) ;
#49563=ORIENTED_EDGE ( 'NONE', *, *, #28230, .F. ) ;
#49826=DIRECTION ( 'NONE',  ( 0.000000000000000000, 0.2617529984165031243, 0.9651348961777157509 ) ) ;
#50182=CARTESIAN_POINT ( 'NONE',  ( -16.88328101497759448, 63.08570056202644594, -213.1263908404952474 ) ) ;
#50300=CARTESIAN_POINT ( 'NONE',  ( -17.29158576265544411, 63.00812307438908988, -211.8292821411627074 ) ) ;
#50419=AXIS2_PLACEMENT_3D ( 'NONE', #190343, #131632, #135469 ) ;
#50473=VERTEX_POINT ( 'NONE', #163262 ) ;
#50778=VERTEX_POINT ( 'NONE', #54832 ) ;
#51430=CIRCLE ( 'NONE', #247263, 0.09999999999999939493 ) ;
#51445=ADVANCED_FACE ( 'NONE', ( #106470 ), #92065, .F. ) ;
#51500=ADVANCED_BREP_SHAPE_REPRESENTATION ( '', ( #198479, #2425 ), #210534 ) ;
#51776=DIRECTION ( 'NONE',  ( 0.000000000000000000, -0.2617529984165031243, -0.9651348961777157509 ) ) ;
#51803=CARTESIAN_POINT ( 'NONE',  ( 20.09999999999999787, 63.27875933230978234, -213.1799721866121047 ) ) ;
#51813=CARTESIAN_POINT ( 'NONE',  ( -16.81744102076748959, 63.08573235307424198, -213.1276215869287967 ) ) ;
#51871=EDGE_CURVE ( 'NONE', #99952, #155667, #71293, .T. ) ;
#51883=VERTEX_POINT ( 'NONE', #214296 ) ;
#51938=AXIS2_PLACEMENT_3D ( 'NONE', #123900, #199600, #97869 ) ;
#52079=FACE_OUTER_BOUND ( 'NONE', #42683, .T. ) ;
#52591=ORIENTED_EDGE ( 'NONE', *, *, #237248, .F. ) ;
#52615=ORIENTED_EDGE ( 'NONE', *, *, #219697, .T. ) ;
#52738=CARTESIAN_POINT ( 'NONE',  ( -16.94107738177415357, 60.85118289042637940, -221.1214263997032390 ) ) ;
#52821=CARTESIAN_POINT ( 'NONE',  ( -16.80100426158792715, 60.95459208743462654, -221.0117235116689756 ) ) ;
#52841=CARTESIAN_POINT ( 'NONE',  ( 18.39999999999999503, 62.23844973457045882, -209.3750075427748527 ) ) ;
#52937=UNCERTAINTY_MEASURE_WITH_UNIT (LENGTH_MEASURE( 1.000000000000000082E-05 ), #226677, 'distance_accuracy_value', 'NONE');
#52938=DIRECTION ( 'NONE',  ( -0.5932847527679298016, -0.7769265190100953511, 0.2107092456252275259 ) ) ;
#53103=CARTESIAN_POINT ( 'NONE',  ( -18.35668295345803713, 62.50563584222673796, -209.4474707446456421 ) ) ;
#53308=DIRECTION ( 'NONE',  ( 1.073024830501117725E-15, 0.2617529984165031243, 0.9651348961777157509 ) ) ;
#53578=DIRECTION ( 'NONE',  ( 1.186688945009010077E-16, 0.9651348961777157509, -0.2617529984165031243 ) ) ;
#53717=LINE ( 'NONE', #193241, #216884 ) ;
#53741=EDGE_LOOP ( 'NONE', ( #224840, #255824, #127528, #220209, #226576, #180089 ) ) ;
#53772=DIRECTION ( 'NONE',  ( -1.000000000000000000, -0.000000000000000000, -0.000000000000000000 ) ) ;
#54642=ORIENTED_EDGE ( 'NONE', *, *, #11113, .F. ) ;
#54667=EDGE_CURVE ( 'NONE', #211757, #236891, #111209, .T. ) ;
#54832=CARTESIAN_POINT ( 'NONE',  ( -16.87683809663752399, 62.98531230502843670, -213.8799296553602005 ) ) ;
#55099=CARTESIAN_POINT ( 'NONE',  ( -15.15766958671843412, 62.18838770701754015, -218.4972640811180611 ) ) ;
#55569=ORIENTED_EDGE ( 'NONE', *, *, #5808, .T. ) ;
#55609=DIRECTION ( 'NONE',  ( 0.000000000000000000, -0.9651348961777157509, 0.2617529984165031243 ) ) ;
#55915=CARTESIAN_POINT ( 'NONE',  ( -17.22361732159831860, 60.22314076454453868, -222.1729100509217858 ) ) ;
#56154=CARTESIAN_POINT ( 'NONE',  ( -16.86733706339143524, 63.08420242447057547, -213.0721725863693905 ) ) ;
#56296=LINE ( 'NONE', #251941, #161264 ) ;
#56367=COLOUR_RGB ( '', 0.40784314, 0.44705882, 0.49803922) ;
#56378=CARTESIAN_POINT ( 'NONE',  ( -16.85722902420173241, 63.05548745535527644, -213.2391404860300952 ) ) ;
#56759=VECTOR ( 'NONE', #192480, 1000.000000000000114 ) ;
#56841=DIRECTION ( 'NONE',  ( -0.000000000000000000, -0.2617529984165031243, -0.9651348961777157509 ) ) ;
#56864=CARTESIAN_POINT ( 'NONE',  ( -16.83199318825828428, 63.07236900629889220, -213.2508343276289793 ) ) ;
#56977=CARTESIAN_POINT ( 'NONE',  ( -16.93302609847409457, 60.87765233411752774, -221.0909021287161806 ) ) ;
#57157=CARTESIAN_POINT ( 'NONE',  ( -18.40000000000000213, 59.45845889640172288, -220.6830127366588101 ) ) ;
#57201=CARTESIAN_POINT ( 'NONE',  ( -16.87036670365549895, 60.86740053880574663, -221.1564527318009254 ) ) ;
#57291=DIRECTION ( 'NONE',  ( 0.000000000000000000, 0.2617529984165031243, 0.9651348961777157509 ) ) ;
#57339=DIRECTION ( 'NONE',  ( 0.7071067811865462405, 0.6824534298470383842, -0.1850873201762212872 ) ) ;
#57388=EDGE_CURVE ( 'NONE', #50778, #135659, #140842, .T. ) ;
#57404=EDGE_CURVE ( 'NONE', #88284, #39258, #42467, .T. ) ;
#57501=ORIENTED_EDGE ( 'NONE', *, *, #170186, .F. ) ;
#57565=CARTESIAN_POINT ( 'NONE',  ( -16.97048361161167307, 62.95718135765960000, -213.6016144441782387 ) ) ;
#57662=FACE_OUTER_BOUND ( 'NONE', #33484, .T. ) ;
#57714=CARTESIAN_POINT ( 'NONE',  ( 12.60053434924910754, 62.27203542310181916, -218.2690822304508913 ) ) ;
#58066=CARTESIAN_POINT ( 'NONE',  ( -16.94878442675512176, 60.88907946405466731, -221.0676920639221805 ) ) ;
#58160=CARTESIAN_POINT ( 'NONE',  ( -16.81931177881022776, 63.07818495933808833, -213.2051305120939446 ) ) ;
#58231=VECTOR ( 'NONE', #218303, 1000.000000000000000 ) ;
#58270=CARTESIAN_POINT ( 'NONE',  ( -16.94445028196808778, 60.88759175473954599, -221.0718995934454938 ) ) ;
#58353=VERTEX_POINT ( 'NONE', #45723 ) ;
#58368=DIRECTION ( 'NONE',  ( -1.000000000000000000, -0.000000000000000000, 0.000000000000000000 ) ) ;
#58405=CARTESIAN_POINT ( 'NONE',  ( 18.39999999999999503, 59.20211495293902004, -220.5705723384363921 ) ) ;
#58822=EDGE_CURVE ( 'NONE', #20388, #186519, #200009, .T. ) ;
#58839=CARTESIAN_POINT ( 'NONE',  ( -16.94226253665225457, 63.00806118293792224, -213.4140105000608116 ) ) ;
#59015=VECTOR ( 'NONE', #38198, 1000.000000000000000 ) ;
#59102=VECTOR ( 'NONE', #168043, 1000.000000000000000 ) ;
#59233=DIRECTION ( 'NONE',  ( -1.000000000000000000, 1.145314911736513911E-16, -3.106193895438251633E-17 ) ) ;
#59273=ORIENTED_EDGE ( 'NONE', *, *, #241537, .F. ) ;
#59344=CARTESIAN_POINT ( 'NONE',  ( -18.40000000000000213, 61.62651781180419874, -212.6889521952982420 ) ) ;
#59370=DIRECTION ( 'NONE',  ( -0.000000000000000000, 0.2617529984165031243, 0.9651348961777157509 ) ) ;
#59559=CARTESIAN_POINT ( 'NONE',  ( -16.92973740335330390, 63.05938405906327660, -213.0623915549271601 ) ) ;
#59660=EDGE_CURVE ( 'NONE', #145413, #250736, #122439, .T. ) ;
#59735=DIRECTION ( 'NONE',  ( 0.000000000000000000, -0.2617529984165031243, -0.9651348961777157509 ) ) ;
#59747=DIRECTION ( 'NONE',  ( -0.000000000000000000, 0.2617529984165031243, 0.9651348961777157509 ) ) ;
#59813=CARTESIAN_POINT ( 'NONE',  ( -14.00000000000000178, 62.10905854918435409, -217.1108499610990918 ) ) ;
#59853=CARTESIAN_POINT ( 'NONE',  ( 23.24999999999999645, 62.02748777246247869, -221.3368380802343722 ) ) ;
#60239=CARTESIAN_POINT ( 'NONE',  ( -16.89935556175753106, 62.95755809683543447, -213.6002253325821698 ) ) ;
#60284=CARTESIAN_POINT ( 'NONE',  ( 12.84233041328157476, 62.18838770701750462, -218.4972640811180611 ) ) ;
#60322=DIRECTION ( 'NONE',  ( 0.000000000000000000, 0.9651348961777379554, -0.2617529984164210233 ) ) ;
#60457=CARTESIAN_POINT ( 'NONE',  ( -23.25000000000000355, 67.23581240663841641, -214.2531594801197627 ) ) ;
#60475=CARTESIAN_POINT ( 'NONE',  ( -16.93262454970419384, 63.05570051748338045, -213.0396161178616694 ) ) ;
#60501=VECTOR ( 'NONE', #128617, 1000.000000000000000 ) ;
#60516=CARTESIAN_POINT ( 'NONE',  ( -16.94165728009534888, 63.05992920170000104, -213.0780854433903642 ) ) ;
#60572=AXIS2_PLACEMENT_3D ( 'NONE', #222985, #84729, #43086 ) ;
#60791=VECTOR ( 'NONE', #162012, 1000.000000000000000 ) ;
#61256=ORIENTED_EDGE ( 'NONE', *, *, #57404, .F. ) ;
#61584=CARTESIAN_POINT ( 'NONE',  ( 13.43443725621852813, 62.06390979127201746, -218.8186321886647931 ) ) ;
#61632=DIRECTION ( 'NONE',  ( -1.000000000000000000, -0.000000000000000000, 0.000000000000000000 ) ) ;
#61652=ORIENTED_EDGE ( 'NONE', *, *, #182148, .F. ) ;
#61776=CARTESIAN_POINT ( 'NONE',  ( -16.93415306273742260, 63.05742080263221538, -213.0577167727462040 ) ) ;
#62115=PRESENTATION_STYLE_ASSIGNMENT (( #103770 ) ) ;
#62176=CARTESIAN_POINT ( 'NONE',  ( -16.86445178670725653, 63.08462010037012391, -213.0850694278881008 ) ) ;
#62177=ADVANCED_FACE ( 'NONE', ( #153083 ), #36976, .T. ) ;
#62327=DIRECTION ( 'NONE',  ( -0.8049926720990043805, 0.5725998182664988612, -0.1552940629517997051 ) ) ;
#62492=DIRECTION ( 'NONE',  ( 0.000000000000000000, 0.2617529984165031243, 0.9651348961777157509 ) ) ;
#62634=ORIENTED_EDGE ( 'NONE', *, *, #139703, .T. ) ;
#62828=CARTESIAN_POINT ( 'NONE',  ( 15.74999999999999645, 62.59162599727320497, -217.2417264603073477 ) ) ;
#62839=DIRECTION ( 'NONE',  ( -1.000000000000000000, 0.000000000000000000, 0.000000000000000000 ) ) ;
#62865=CARTESIAN_POINT ( 'NONE',  ( 14.56326696814971555, 62.06361769656462712, -218.8193597571736007 ) ) ;
#62883=DIRECTION ( 'NONE',  ( 0.5932847527679309119, 0.7769265190100945739, -0.2107092456252266377 ) ) ;
#62912=VERTEX_POINT ( 'NONE', #84705 ) ;
#63063=EDGE_CURVE ( 'NONE', #163271, #19038, #209838, .T. ) ;
#63314=CARTESIAN_POINT ( 'NONE',  ( -16.89268316805466341, 60.93619025550653134, -221.0468289635910537 ) ) ;
#63371=( LENGTH_UNIT ( ) NAMED_UNIT ( * ) SI_UNIT ( .MILLI., .METRE. ) );
#63521=CARTESIAN_POINT ( 'NONE',  ( -16.88783316861822925, 60.96612568567729085, -220.9430291400472868 ) ) ;
#63648=ORIENTED_EDGE ( 'NONE', *, *, #197823, .F. ) ;
#63660=CARTESIAN_POINT ( 'NONE',  ( -16.87851181299898684, 60.93927877302353124, -221.0418550117870780 ) ) ;
#63859=CARTESIAN_POINT ( 'NONE',  ( 18.39999999999999503, 62.50563584222673796, -209.4474707446456421 ) ) ;
#63900=ORIENTED_EDGE ( 'NONE', *, *, #120504, .F. ) ;
#63940=EDGE_CURVE ( 'NONE', #19038, #127095, #196734, .T. ) ;
#64229=AXIS2_PLACEMENT_3D ( 'NONE', #14357, #93860, #155159 ) ;
#64325=LINE ( 'NONE', #5601, #186311 ) ;
#64354=CARTESIAN_POINT ( 'NONE',  ( -16.93234230245721861, 63.05702038518566610, -213.0496990854739749 ) ) ;
#64534=CARTESIAN_POINT ( 'NONE',  ( -33.72168855820452649, 58.57934086597919077, -223.9244941873113817 ) ) ;
#64676=CARTESIAN_POINT ( 'NONE',  ( -16.87683809663752399, 60.93935776605891164, -221.0417277355860790 ) ) ;
#64732=DIRECTION ( 'NONE',  ( -1.000000000000000000, -0.000000000000000000, -0.000000000000000000 ) ) ;
#64798=VECTOR ( 'NONE', #199544, 1000.000000000000000 ) ;
#65043=SURFACE_STYLE_FILL_AREA ( #147143 ) ;
#65044=FACE_OUTER_BOUND ( 'NONE', #236591, .T. ) ;
#65205=ORIENTED_EDGE ( 'NONE', *, *, #210701, .T. ) ;
#65213=DIRECTION ( 'NONE',  ( -1.000000000000000000, -1.541976423090492636E-14, 0.000000000000000000 ) ) ;
#65393=CARTESIAN_POINT ( 'NONE',  ( 14.45963434102923273, 62.93961911720151647, -215.5706779233118766 ) ) ;
#65456=( BOUNDED_SURFACE ( )  B_SPLINE_SURFACE ( 3, 2, ( 
 ( #139195, #42687, #3549 ),
 ( #118388, #141774, #182209 ),
 ( #199203, #23151, #162647 ),
 ( #19276, #123513, #43970 ),
 ( #40156, #20580, #242165 ),
 ( #63521, #222582, #41428 ),
 ( #179651, #955, #200484 ),
 ( #143054, #203035, #24437 ),
 ( #80493, #160093, #120970 ),
 ( #103916, #183489, #178376 ) ),
 .UNSPECIFIED., .F., .F., .T. ) 
 B_SPLINE_SURFACE_WITH_KNOTS ( ( 4, 2, 2, 2, 4 ),
 ( 3, 3 ),
 ( 0.002161241639767781664, 0.002579950749617448968, 0.002789305304542282621, 0.002893982582004699447, 0.002998659859467116707 ),
 ( 0.000000000000000000, 1.000000000000000000 ),
 .UNSPECIFIED. ) 
 GEOMETRIC_REPRESENTATION_ITEM ( )  RATIONAL_B_SPLINE_SURFACE ( (
 ( 1.000000000000000000, 0.7071067811864784058, 1.000000000000000000),
 ( 1.000000000000000000, 0.7632447400667680126, 1.000000000000000000),
 ( 1.000000000000000000, 0.8158073005103720909, 1.000000000000000000),
 ( 1.000000000000000000, 0.8906973462398690700, 1.000000000000000000),
 ( 1.000000000000000000, 0.9149408947801378478, 1.000000000000000000),
 ( 1.000000000000000000, 0.9493368785274739485, 1.000000000000000000),
 ( 1.000000000000000000, 0.9605194247157018417, 1.000000000000000000),
 ( 1.000000000000000000, 0.9803630264780553993, 1.000000000000000000),
 ( 1.000000000000000000, 0.9900844824271457512, 1.000000000000000000),
 ( 1.000000000000000000, 0.9894588281429201881, 1.000000000000000000) ) ) 
 REPRESENTATION_ITEM ( '' )  SURFACE ( )  );
#66070=VERTEX_POINT ( 'NONE', #147761 ) ;
#66175=CARTESIAN_POINT ( 'NONE',  ( -15.66061380678751824, 62.72888572355476811, -216.6946536606585028 ) ) ;
#66277=ORIENTED_EDGE ( 'NONE', *, *, #37348, .T. ) ;
#66347=ORIENTED_EDGE ( 'NONE', *, *, #35781, .T. ) ;
#66556=CARTESIAN_POINT ( 'NONE',  ( -12.47155713865592475, 62.33593033127510097, -218.0864590324957248 ) ) ;
#66726=CARTESIAN_POINT ( 'NONE',  ( 15.15590539855246277, 62.18784473894375964, -218.4987171750605057 ) ) ;
#66925=VERTEX_POINT ( 'NONE', #256112 ) ;
#67123=VERTEX_POINT ( 'NONE', #246880 ) ;
#67229=ORIENTED_EDGE ( 'NONE', *, *, #116568, .F. ) ;
#67284=CARTESIAN_POINT ( 'NONE',  ( -16.92507428761698662, 63.06913787792631609, -213.1888086875385966 ) ) ;
#67352=LINE ( 'NONE', #148166, #60501 ) ;
#67680=DIRECTION ( 'NONE',  ( 0.2834754621636438876, 0.5133902848552793774, 0.8099827638705180410 ) ) ;
#68000=CARTESIAN_POINT ( 'NONE',  ( 14.87567385445978196, 62.11595298889567118, -218.6870723643519341 ) ) ;
#68338=CARTESIAN_POINT ( 'NONE',  ( 18.39999999999999503, 68.12577260125452483, -210.9717008331155341 ) ) ;
#68343=AXIS2_PLACEMENT_3D ( 'NONE', #187852, #91304, #109558 ) ;
#68347=LINE ( 'NONE', #106154, #164235 ) ;
#68395=DIRECTION ( 'NONE',  ( 1.073024830501117725E-15, -0.2617529984165031243, -0.9651348961777157509 ) ) ;
#68484=CARTESIAN_POINT ( 'NONE',  ( -16.87331047859651179, 60.93935776605891164, -221.0417277355860790 ) ) ;
#68553=FACE_OUTER_BOUND ( 'NONE', #100504, .T. ) ;
#68597=B_SPLINE_CURVE_WITH_KNOTS ( 'NONE', 3,
 ( #73445, #31755, #152990, #232512, #133396, #55099, #175134, #212928, #10436, #110804, #26153, #31312, #209928, #7878, #126525, #106944, #127817, #228201, #70440, #165672, #207359, #30019, #66556, #48267, #105646, #187797 ),
 .UNSPECIFIED., .F., .F.,
 ( 4, 2, 2, 2, 2, 2, 2, 2, 2, 2, 2, 2, 4 ),
 ( 0.005476422646581361256, 0.006160811967703612099, 0.006845201288825863810, 0.007187395949386962343, 0.007529590609948060009, 0.007871785270509157675, 0.008213979931070255341, 0.008556174591631353007, 0.008898369252192450674, 0.009240563912753550074, 0.009582758573314646006, 0.01026714789443683787, 0.01095153721555903147 ),
 .UNSPECIFIED. ) ;
#68645=CARTESIAN_POINT ( 'NONE',  ( -18.34374000495060386, 58.57934086597919077, -223.9244941873113817 ) ) ;
#68725=LINE ( 'NONE', #145675, #70030 ) ;
#68741=ORIENTED_EDGE ( 'NONE', *, *, #7570, .T. ) ;
#68752=CARTESIAN_POINT ( 'NONE',  ( -12.30589683808041102, 62.70378344720913333, -216.8024073824997231 ) ) ;
#68807=ADVANCED_FACE ( 'NONE', ( #88203 ), #205601, .F. ) ;
#68841=DIRECTION ( 'NONE',  ( 0.000000000000000000, -0.9651348961777157509, 0.2617529984165031243 ) ) ;
#68919=EDGE_LOOP ( 'NONE', ( #173677, #208001, #164407, #5174, #81016 ) ) ;
#68934=DIRECTION ( 'NONE',  ( 0.000000000000000000, 0.9651348961777157509, -0.2617529984165031243 ) ) ;
#69078=DIRECTION ( 'NONE',  ( 0.000000000000000000, 0.2617529984165031243, 0.9651348961777157509 ) ) ;
#69204=LINE ( 'NONE', #7931, #127961 ) ;
#69765=CARTESIAN_POINT ( 'NONE',  ( -17.27223548803355513, 60.22175817953561960, -222.1770843993087396 ) ) ;
#69844=DIRECTION ( 'NONE',  ( -1.020425574104004196E-15, -0.2617529984165031243, -0.9651348961777157509 ) ) ;
#69909=CARTESIAN_POINT ( 'NONE',  ( -16.94107738177414291, 63.04990807712500356, -213.0142932718104021 ) ) ;
#70030=VECTOR ( 'NONE', #226485, 1000.000000000000114 ) ;
#70131=VECTOR ( 'NONE', #228932, 1000.000000000000000 ) ;
#70141=PLANE ( 'NONE',  #155915 ) ;
#70322=VERTEX_POINT ( 'NONE', #101052 ) ;
#70334=LINE ( 'NONE', #187699, #120272 ) ;
#70385=EDGE_LOOP ( 'NONE', ( #19992, #237081, #100657, #233698, #17691 ) ) ;
#70440=CARTESIAN_POINT ( 'NONE',  ( -13.12432614554022869, 62.11595298889567118, -218.6870723643518772 ) ) ;
#70468=AXIS2_PLACEMENT_3D ( 'NONE', #250117, #68934, #148460 ) ;
#70557=EDGE_CURVE ( 'NONE', #229612, #91602, #112675, .T. ) ;
#70566=CARTESIAN_POINT ( 'NONE',  ( 12.42718393586867087, 62.77476515014583924, -216.4875458411300713 ) ) ;
#70889=EDGE_CURVE ( 'NONE', #107985, #238512, #224576, .T. ) ;
#71092=AXIS2_PLACEMENT_3D ( 'NONE', #72503, #152048, #12536 ) ;
#71157=LINE ( 'NONE', #112831, #70131 ) ;
#71293=CIRCLE ( 'NONE', #192104, 0.09999999999999543976 ) ;
#71385=CARTESIAN_POINT ( 'NONE',  ( -20.65000000000000568, 64.19947762500697763, -225.4487242757812737 ) ) ;
#71392=CARTESIAN_POINT ( 'NONE',  ( -18.40000000000000213, 62.48575673152180343, -209.5207689439494345 ) ) ;
#71407=LINE ( 'NONE', #153541, #180864 ) ;
#71555=ADVANCED_FACE ( 'NONE', ( #204066 ), #161113, .F. ) ;
#71873=FACE_OUTER_BOUND ( 'NONE', #77838, .T. ) ;
#72094=CARTESIAN_POINT ( 'NONE',  ( 23.24999999999999645, 67.23581240663841641, -214.2531594801197627 ) ) ;
#72162=ORIENTED_EDGE ( 'NONE', *, *, #214482, .F. ) ;
#72170=AXIS2_PLACEMENT_3D ( 'NONE', #104464, #5362, #184022 ) ;
#72384=ORIENTED_EDGE ( 'NONE', *, *, #2745, .F. ) ;
#72503=CARTESIAN_POINT ( 'NONE',  ( -23.25000000000000355, 64.19947762500697763, -225.4487242757812737 ) ) ;
#72505=ORIENTED_EDGE ( 'NONE', *, *, #33141, .F. ) ;
#72586=VECTOR ( 'NONE', #188104, 1000.000000000000000 ) ;
#73009=CARTESIAN_POINT ( 'NONE',  ( 20.73486653747088226, 63.54522198573869929, -221.7484608313106094 ) ) ;
#73037=EDGE_LOOP ( 'NONE', ( #165488, #130423, #142646, #240095 ) ) ;
#73045=CARTESIAN_POINT ( 'NONE',  ( -16.77977881697927387, 60.94561573421638201, -221.0316353316906088 ) ) ;
#73290=AXIS2_PLACEMENT_3D ( 'NONE', #214812, #96135, #142640 ) ;
#73445=CARTESIAN_POINT ( 'NONE',  ( -15.75000000000000355, 62.59162599727320497, -217.2417264603073477 ) ) ;
#73756=AXIS2_PLACEMENT_3D ( 'NONE', #3618, #62327, #141847 ) ;
#74054=VERTEX_POINT ( 'NONE', #124331 ) ;
#74056=ORIENTED_EDGE ( 'NONE', *, *, #46303, .F. ) ;
#74137=UNCERTAINTY_MEASURE_WITH_UNIT (LENGTH_MEASURE( 1.000000000000000082E-05 ), #63371, 'distance_accuracy_value', 'NONE');
#74198=FACE_OUTER_BOUND ( 'NONE', #1217, .T. ) ;
#74635=ORIENTED_EDGE ( 'NONE', *, *, #129149, .T. ) ;
#74783=EDGE_CURVE ( 'NONE', #62912, #118476, #41772, .T. ) ;
#74822=DIRECTION ( 'NONE',  ( -1.000000000000000000, -1.594516344651357984E-15, 4.324467345337419894E-16 ) ) ;
#74845=DIRECTION ( 'NONE',  ( 0.000000000000000000, -0.9651348961777157509, 0.2617529984165031243 ) ) ;
#74848=EDGE_CURVE ( 'NONE', #39830, #237838, #117335, .T. ) ;
#75059=CARTESIAN_POINT ( 'NONE',  ( 18.39999999999999503, 59.20211495293902004, -220.5705723384363921 ) ) ;
#75110=CARTESIAN_POINT ( 'NONE',  ( 21.72449340488910252, 59.72708471423849375, -224.2357723256170061 ) ) ;
#75304=ORIENTED_EDGE ( 'NONE', *, *, #141329, .F. ) ;
#75347=ORIENTED_EDGE ( 'NONE', *, *, #74783, .F. ) ;
#75505=CARTESIAN_POINT ( 'NONE',  ( 23.04999999999999716, 61.13752757784637026, -224.6182967272386009 ) ) ;
#75534=CARTESIAN_POINT ( 'NONE',  ( -18.40000000000000213, 61.34848953995435039, -212.6564661897791098 ) ) ;
#75648=AXIS2_PLACEMENT_3D ( 'NONE', #46398, #188487, #127240 ) ;
#75669=VERTEX_POINT ( 'NONE', #244129 ) ;
#75872=VERTEX_POINT ( 'NONE', #35410 ) ;
#75967=CARTESIAN_POINT ( 'NONE',  ( -16.97683809663752186, 62.88879881541066652, -213.8537543555185607 ) ) ;
#76089=ORIENTED_EDGE ( 'NONE', *, *, #6717, .T. ) ;
#76232=CARTESIAN_POINT ( 'NONE',  ( -16.89268316805465986, 63.08557629953710943, -213.1216189793661329 ) ) ;
#76532=VECTOR ( 'NONE', #69078, 1000.000000000000000 ) ;
#76563=CARTESIAN_POINT ( 'NONE',  ( -16.93230518875208546, 60.87094908132711168, -221.1000775826128972 ) ) ;
#76683=DIRECTION ( 'NONE',  ( -0.000000000000000000, 0.2617529984165031243, 0.9651348961777157509 ) ) ;
#76715=EDGE_CURVE ( 'NONE', #75669, #43158, #39915, .T. ) ;
#76737=ORIENTED_EDGE ( 'NONE', *, *, #30754, .T. ) ;
#76966=ORIENTED_EDGE ( 'NONE', *, *, #135985, .F. ) ;
#77013=CARTESIAN_POINT ( 'NONE',  ( -16.86337532320260735, 63.08270373490941552, -213.0243021242677628 ) ) ;
#77094=EDGE_LOOP ( 'NONE', ( #244740, #247311, #184479, #218628 ) ) ;
#77141=CARTESIAN_POINT ( 'NONE',  ( -16.84419801905645997, 63.08063082738696181, -213.1464319176388642 ) ) ;
#77162=VECTOR ( 'NONE', #89725, 1000.000000000000000 ) ;
#77226=VERTEX_POINT ( 'NONE', #228178 ) ;
#77291=CARTESIAN_POINT ( 'NONE',  ( 18.39999999999999503, 59.20211495293902004, -220.5705723384363921 ) ) ;
#77335=ADVANCED_FACE ( 'NONE', ( #52079 ), #36414, .F. ) ;
#77411=ORIENTED_EDGE ( 'NONE', *, *, #253038, .F. ) ;
#77430=VERTEX_POINT ( 'NONE', #97609 ) ;
#77605=AXIS2_PLACEMENT_3D ( 'NONE', #5824, #68395, #7116 ) ;
#77838=EDGE_LOOP ( 'NONE', ( #212345, #139945, #221126, #195340 ) ) ;
#77965=EDGE_CURVE ( 'NONE', #74054, #20388, #163536, .T. ) ;
#78004=CIRCLE ( 'NONE', #161424, 0.5000000000000004441 ) ;
#78290=CARTESIAN_POINT ( 'NONE',  ( -16.88460203013674388, 63.08529900177730099, -213.1110381636136424 ) ) ;
#78298=ORIENTED_EDGE ( 'NONE', *, *, #157075, .T. ) ;
#78312=( BOUNDED_SURFACE ( )  B_SPLINE_SURFACE ( 3, 2, ( 
 ( #240453, #158384, #80051 ),
 ( #159637, #102186, #140042 ),
 ( #121804, #40999, #237882 ),
 ( #241734, #120533, #181768 ) ),
 .UNSPECIFIED., .F., .F., .F. ) 
 B_SPLINE_SURFACE_WITH_KNOTS ( ( 4, 4 ),
 ( 3, 3 ),
 ( 0.3000847527772385059, 0.5552748953338751958 ),
 ( 0.000000000000000000, 1.000000000000000000 ),
 .UNSPECIFIED. ) 
 GEOMETRIC_REPRESENTATION_ITEM ( )  RATIONAL_B_SPLINE_SURFACE ( (
 ( 1.000000000000000000, 0.9152888060719372998, 1.000000000000000000),
 ( 1.000000000000000000, 0.9104333467450547168, 1.000000000000000000),
 ( 1.000000000000000000, 0.9035312726220219304, 1.000000000000000000),
 ( 1.000000000000000000, 0.8946697475932521293, 1.000000000000000000) ) ) 
 REPRESENTATION_ITEM ( '' )  SURFACE ( )  );
#78328=( BOUNDED_SURFACE ( )  B_SPLINE_SURFACE ( 3, 2, ( 
 ( #102536, #238228, #240811 ),
 ( #200399, #41350, #183407 ),
 ( #62176, #122148, #59559 ),
 ( #21772, #199112, #101238 ) ),
 .UNSPECIFIED., .F., .F., .F. ) 
 B_SPLINE_SURFACE_WITH_KNOTS ( ( 4, 4 ),
 ( 3, 3 ),
 ( 0.0008258556059633668459, 0.0009616864997632829570 ),
 ( 0.000000000000000000, 1.000000000000000000 ),
 .UNSPECIFIED. ) 
 GEOMETRIC_REPRESENTATION_ITEM ( )  RATIONAL_B_SPLINE_SURFACE ( (
 ( 1.000000000000000000, 0.9152888060719409635, 1.000000000000000000),
 ( 1.000000000000000000, 0.9327727094138329456, 1.000000000000000000),
 ( 1.000000000000000000, 0.9369023509258374016, 1.000000000000000000),
 ( 1.000000000000000000, 0.9246339933864329286, 1.000000000000000000) ) ) 
 REPRESENTATION_ITEM ( '' )  SURFACE ( )  );
#78515=CARTESIAN_POINT ( 'NONE',  ( -16.80070461188017816, 63.08652707989409691, -213.1246912725079881 ) ) ;
#78613=ORIENTED_EDGE ( 'NONE', *, *, #5494, .F. ) ;
#78789=CARTESIAN_POINT ( 'NONE',  ( -16.90128866880176872, 63.08538694504799338, -213.1143938039259069 ) ) ;
#79056=DIRECTION ( 'NONE',  ( -0.000000000000000000, 0.2617529984165031243, 0.9651348961777157509 ) ) ;
#79089=VECTOR ( 'NONE', #97322, 1000.000000000000000 ) ;
#79090=LINE ( 'NONE', #238172, #37428 ) ;
#79712=EDGE_LOOP ( 'NONE', ( #162989, #193100 ) ) ;
#79792=CARTESIAN_POINT ( 'NONE',  ( -18.38639463286148867, 58.57254856461742065, -223.9226520559630558 ) ) ;
#79877=FACE_OUTER_BOUND ( 'NONE', #131235, .T. ) ;
#80018=CARTESIAN_POINT ( 'NONE',  ( -16.94445028196807002, 63.05630424923659660, -213.0754291771441729 ) ) ;
#80051=CARTESIAN_POINT ( 'NONE',  ( -16.87036670365548474, 63.08160062417908165, -212.9922606024214815 ) ) ;
#80055=CARTESIAN_POINT ( 'NONE',  ( -16.94052228080552069, 63.06128592552281731, -213.0791574514314561 ) ) ;
#80184=CARTESIAN_POINT ( 'NONE',  ( -16.89797118371629736, 60.89104750934725985, -221.1190723775698643 ) ) ;
#80280=CARTESIAN_POINT ( 'NONE',  ( -16.78493211734301482, 63.08610022504905146, -213.1421742787360074 ) ) ;
#80289=ORIENTED_EDGE ( 'NONE', *, *, #182148, .T. ) ;
#80493=CARTESIAN_POINT ( 'NONE',  ( -16.80891096016323871, 60.93473447329584758, -221.0587747272457193 ) ) ;
#80503=ADVANCED_FACE ( 'NONE', ( #183413 ), #204241, .F. ) ;
#80639=CARTESIAN_POINT ( 'NONE',  ( -16.88560720703333473, 60.93831840527001020, -221.0434021371021345 ) ) ;
#80779=DIRECTION ( 'NONE',  ( -1.000000000000000000, 0.000000000000000000, 0.000000000000000000 ) ) ;
#80785=CARTESIAN_POINT ( 'NONE',  ( 18.54999999999999716, 62.09751964147213243, -221.3558313336858703 ) ) ;
#80959=CARTESIAN_POINT ( 'NONE',  ( 20.27550659511088682, 60.75776438711819338, -224.5153016389302536 ) ) ;
#81016=ORIENTED_EDGE ( 'NONE', *, *, #125325, .F. ) ;
#81082=CARTESIAN_POINT ( 'NONE',  ( -18.34374000495060386, 58.57934086597919077, -223.9244941873113817 ) ) ;
#81663=CARTESIAN_POINT ( 'NONE',  ( -16.94062896051973865, 60.88569912951715679, -221.0763738239286340 ) ) ;
#81880=VECTOR ( 'NONE', #74845, 1000.000000000000000 ) ;
#81889=ORIENTED_EDGE ( 'NONE', *, *, #148382, .T. ) ;
#81970=CARTESIAN_POINT ( 'NONE',  ( 20.73486653747088582, 63.54522198573869929, -221.7484608313106094 ) ) ;
#82357=CARTESIAN_POINT ( 'NONE',  ( 13.43663047529819288, 62.93307127222839625, -215.6135269849708891 ) ) ;
#82395=CARTESIAN_POINT ( 'NONE',  ( 14.22821877134047774, 62.03415779510191896, -218.8921516991029819 ) ) ;
#82627=ORIENTED_EDGE ( 'NONE', *, *, #241584, .F. ) ;
#82843=CARTESIAN_POINT ( 'NONE',  ( -16.85312964099709276, 63.05615751446485007, -213.3757143580369302 ) ) ;
#82889=ORIENTED_EDGE ( 'NONE', *, *, #77965, .F. ) ;
#82912=EDGE_CURVE ( 'NONE', #209093, #14211, #109052, .T. ) ;
#83052=ORIENTED_EDGE ( 'NONE', *, *, #255740, .T. ) ;
#83056=FACE_OUTER_BOUND ( 'NONE', #218755, .T. ) ;
#83232=CARTESIAN_POINT ( 'NONE',  ( -16.78270389226383230, 63.08596654800939518, -213.1367957079248185 ) ) ;
#83431=ADVANCED_FACE ( 'NONE', ( #79877 ), #219401, .F. ) ;
#83455=ADVANCED_FACE ( 'NONE', ( #1638 ), #176465, .F. ) ;
#83463=ORIENTED_EDGE ( 'NONE', *, *, #224783, .T. ) ;
#83517=VERTEX_POINT ( 'NONE', #36969 ) ;
#83550=EDGE_CURVE ( 'NONE', #180612, #22197, #98129, .T. ) ;
#83862=CARTESIAN_POINT ( 'NONE',  ( -16.93433913041102912, 63.05405028161031566, -213.0305799143420984 ) ) ;
#83992=DIRECTION ( 'NONE',  ( -1.652117596168391700E-15, 0.9651348961777157509, -0.2617529984165031243 ) ) ;
#84015=ADVANCED_FACE ( 'NONE', ( #45626 ), #202127, .F. ) ;
#84064=B_SPLINE_CURVE_WITH_KNOTS ( 'NONE', 3,
 ( #202379, #238947, #1597, #216796, #57714, #60284, #139821, #38188, #240238, #61584, #220664, #42040, #181551, #2873, #82395, #241506, #62865, #104526, #68000, #144951, #66726, #164547, #204926, #84961, #107120, #143678 ),
 .UNSPECIFIED., .F., .F.,
 ( 4, 2, 2, 2, 2, 2, 2, 2, 2, 2, 2, 2, 4 ),
 ( 0.005476422646581336103, 0.006160811967703527965, 0.006845201288825720695, 0.007187395949386819229, 0.007529590609947917762, 0.007871785270509017163, 0.008213979931070114829, 0.008556174591631212495, 0.008898369252192311896, 0.009240563912753411296, 0.009582758573314508962, 0.01026714789443677021, 0.01095153721555903320 ),
 .UNSPECIFIED. ) ;
#84470=ORIENTED_EDGE ( 'NONE', *, *, #194505, .T. ) ;
#84674=ORIENTED_EDGE ( 'NONE', *, *, #160647, .T. ) ;
#84705=CARTESIAN_POINT ( 'NONE',  ( 18.54999999999999716, 63.08573235307424198, -213.1276215869287398 ) ) ;
#84729=DIRECTION ( 'NONE',  ( -1.073024830501117725E-15, -0.2617529984165031243, -0.9651348961777157509 ) ) ;
#84921=CARTESIAN_POINT ( 'NONE',  ( 15.31784899511109010, 62.84948463577723032, -216.1128043527995999 ) ) ;
#84935=EDGE_CURVE ( 'NONE', #31477, #87486, #250567, .T. ) ;
#84961=CARTESIAN_POINT ( 'NONE',  ( 15.70340296795548873, 62.46518123923912214, -217.6854569796042256 ) ) ;
#85077=DIRECTION ( 'NONE',  ( -0.000000000000000000, 0.2617529984165031243, 0.9651348961777157509 ) ) ;
#85347=CARTESIAN_POINT ( 'NONE',  ( -16.94225986326251032, 61.01702495231255341, -220.7553535118148602 ) ) ;
#85560=STYLED_ITEM ( 'NONE', ( #106722 ), #198479 ) ;
#85695=CARTESIAN_POINT ( 'NONE',  ( -12.25000000000000000, 62.62192211835339606, -217.1300186905772307 ) ) ;
#86159=AXIS2_PLACEMENT_3D ( 'NONE', #236183, #211496, #135787 ) ;
#86449=DIRECTION ( 'NONE',  ( -0.000000000000000000, 0.2617529984165031243, 0.9651348961777157509 ) ) ;
#86718=ORIENTED_EDGE ( 'NONE', *, *, #148157, .T. ) ;
#86791=LINE ( 'NONE', #64676, #3029 ) ;
#86860=AXIS2_PLACEMENT_3D ( 'NONE', #47668, #12438, #69844 ) ;
#87152=FACE_OUTER_BOUND ( 'NONE', #96999, .T. ) ;
#87366=ORIENTED_EDGE ( 'NONE', *, *, #160647, .F. ) ;
#87477=CARTESIAN_POINT ( 'NONE',  ( -16.94107738177414291, 63.04990807712500356, -213.0142932718104021 ) ) ;
#87486=VERTEX_POINT ( 'NONE', #250687 ) ;
#87518=DIRECTION ( 'NONE',  ( -1.073024830501117725E-15, 0.2617529984165031243, 0.9651348961777157509 ) ) ;
#87666=CARTESIAN_POINT ( 'NONE',  ( 20.73486653747088582, 62.65526179112259086, -225.0299194783148664 ) ) ;
#87968=DIRECTION ( 'NONE',  ( 0.7071067811865463515, 0.6824534298470384952, -0.1850873201762213149 ) ) ;
#88185=( BOUNDED_CURVE ( )  B_SPLINE_CURVE ( 3, ( #195341, #16694, #233186, #96196 ),
 .UNSPECIFIED., .F., .F. ) 
 B_SPLINE_CURVE_WITH_KNOTS ( ( 4, 4 ),
 ( 0.3000847527772402823, 0.5517402753107897295 ),
 .UNSPECIFIED. ) 
 CURVE ( )  GEOMETRIC_REPRESENTATION_ITEM ( )  RATIONAL_B_SPLINE_CURVE ( ( 1.000000000000000000, 0.9947294176030464508, 0.9947294176030464508, 1.000000000000000000 ) ) 
 REPRESENTATION_ITEM ( '' )  );
#88203=FACE_OUTER_BOUND ( 'NONE', #53741, .T. ) ;
#88244=CARTESIAN_POINT ( 'NONE',  ( 15.74999999999999645, 62.59162599727320497, -217.2417264603073477 ) ) ;
#88272=CARTESIAN_POINT ( 'NONE',  ( -12.26136940704871847, 62.65035202501400846, -217.0198313409406978 ) ) ;
#88284=VERTEX_POINT ( 'NONE', #142625 ) ;
#88370=CARTESIAN_POINT ( 'NONE',  ( -16.80117486205003274, 63.08576339494070595, -213.1288165000758568 ) ) ;
#88433=AXIS2_PLACEMENT_3D ( 'NONE', #117409, #199538, #256863 ) ;
#89471=DIRECTION ( 'NONE',  ( -1.000000000000000000, 0.000000000000000000, 0.000000000000000000 ) ) ;
#89485=CARTESIAN_POINT ( 'NONE',  ( -23.25000000000000355, 59.20211495293902004, -220.5705723384363921 ) ) ;
#89725=DIRECTION ( 'NONE',  ( -0.000000000000000000, 0.2617529984165031243, 0.9651348961777157509 ) ) ;
#89833=EDGE_LOOP ( 'NONE', ( #15102, #172502, #90429, #241384, #57501 ) ) ;
#90053=PRODUCT_CONTEXT ( 'NONE', #43997, 'mechanical' ) ;
#90209=CARTESIAN_POINT ( 'NONE',  ( 17.74533788810830970, 62.85906666726748426, -210.6453698753407480 ) ) ;
#90221=ORIENTED_EDGE ( 'NONE', *, *, #191194, .T. ) ;
#90429=ORIENTED_EDGE ( 'NONE', *, *, #254698, .F. ) ;
#90460=EDGE_CURVE ( 'NONE', #27216, #31477, #168224, .T. ) ;
#90465=AXIS2_PLACEMENT_3D ( 'NONE', #129692, #87968, #30617 ) ;
#90667=CARTESIAN_POINT ( 'NONE',  ( -16.78493832629888871, 60.94702803318471496, -221.0293550571836363 ) ) ;
#90818=VERTEX_POINT ( 'NONE', #6101 ) ;
#91293=CARTESIAN_POINT ( 'NONE',  ( -16.77779411503079388, 60.94653821389059090, -221.0301460241443010 ) ) ;
#91304=DIRECTION ( 'NONE',  ( 1.186688945009009831E-16, 0.9651348961777157509, -0.2617529984165031243 ) ) ;
#91524=CARTESIAN_POINT ( 'NONE',  ( 16.87683809663749557, 63.08573235307424198, -213.1276215869287967 ) ) ;
#91602=VERTEX_POINT ( 'NONE', #58405 ) ;
#91736=ADVANCED_FACE ( 'NONE', ( #184793 ), #121009, .F. ) ;
#92065=PLANE ( 'NONE',  #37799 ) ;
#92100=ORIENTED_EDGE ( 'NONE', *, *, #191424, .F. ) ;
#92566=VECTOR ( 'NONE', #93741, 1000.000000000000227 ) ;
#92659=DIRECTION ( 'NONE',  ( 0.000000000000000000, 0.9651348961777157509, -0.2617529984165031243 ) ) ;
#93093=CARTESIAN_POINT ( 'NONE',  ( -14.00000000000000178, 62.10905854918435409, -217.1108499610990918 ) ) ;
#93199=VECTOR ( 'NONE', #38622, 1000.000000000000000 ) ;
#93281=EDGE_CURVE ( 'NONE', #180046, #19038, #96089, .T. ) ;
#93336=EDGE_CURVE ( 'NONE', #58353, #133225, #86791, .T. ) ;
#93524=ORIENTED_EDGE ( 'NONE', *, *, #84935, .T. ) ;
#93741=DIRECTION ( 'NONE',  ( -0.5932847527679309119, -0.7769265190100942409, 0.2107092456252278867 ) ) ;
#93821=( GEOMETRIC_REPRESENTATION_CONTEXT ( 3 ) GLOBAL_UNCERTAINTY_ASSIGNED_CONTEXT ( ( #256526 ) ) GLOBAL_UNIT_ASSIGNED_CONTEXT ( ( #102480, #40013, #25561 ) ) REPRESENTATION_CONTEXT ( 'NONE', 'WORKASPACE' ) );
#93860=DIRECTION ( 'NONE',  ( 1.186688945009009831E-16, 0.9651348961777157509, -0.2617529984165031243 ) ) ;
#94067=DIRECTION ( 'NONE',  ( 1.073024830501117725E-15, -0.2617529984165031243, -0.9651348961777157509 ) ) ;
#94123=DIRECTION ( 'NONE',  ( -1.000000000000000000, -0.000000000000000000, 0.000000000000000000 ) ) ;
#94171=CARTESIAN_POINT ( 'NONE',  ( -33.72168855820451938, 60.93935776605888321, -221.0417277355861359 ) ) ;
#94221=CARTESIAN_POINT ( 'NONE',  ( 21.72449340488909897, 62.76341949586993252, -213.0402075299554951 ) ) ;
#94276=VECTOR ( 'NONE', #181804, 1000.000000000000000 ) ;
#94292=VECTOR ( 'NONE', #37359, 1000.000000000000000 ) ;
#94303=ORIENTED_EDGE ( 'NONE', *, *, #2745, .T. ) ;
#94390=VECTOR ( 'NONE', #236523, 1000.000000000000000 ) ;
#94639=PRODUCT_DEFINITION ( 'UNKNOWN', '', #219622, #115799 ) ;
#95347=ADVANCED_FACE ( 'NONE', ( #32737 ), #191798, .T. ) ;
#95605=ADVANCED_FACE ( 'NONE', ( #144611 ), #224155, .F. ) ;
#95608=AXIS2_PLACEMENT_3D ( 'NONE', #99137, #242518, #118743 ) ;
#95758=ORIENTED_EDGE ( 'NONE', *, *, #5808, .F. ) ;
#96060=ORIENTED_EDGE ( 'NONE', *, *, #182661, .T. ) ;
#96089=LINE ( 'NONE', #158683, #202959 ) ;
#96122=VECTOR ( 'NONE', #126041, 1000.000000000000000 ) ;
#96135=DIRECTION ( 'NONE',  ( -0.7071067811865456854, -0.6824534298470390503, 0.1850873201762214815 ) ) ;
#96196=CARTESIAN_POINT ( 'NONE',  ( -18.34374000495059676, 62.50563584222673796, -209.4474707446456421 ) ) ;
#96357=CARTESIAN_POINT ( 'NONE',  ( -16.94107738177415712, 60.85118289042637940, -221.1214263997032106 ) ) ;
#96560=CARTESIAN_POINT ( 'NONE',  ( -16.86379686415369150, 63.08322136712259010, -213.0405382708815409 ) ) ;
#96731=VERTEX_POINT ( 'NONE', #187748 ) ;
#96774=CARTESIAN_POINT ( 'NONE',  ( -16.92280123533710068, 63.03321624328317796, -213.3212588345534186 ) ) ;
#96779=CARTESIAN_POINT ( 'NONE',  ( -18.35663730107557257, 58.57862133557244988, -223.9242990443918302 ) ) ;
#96999=EDGE_LOOP ( 'NONE', ( #147734, #158255, #196085, #131600, #215717, #213427, #22006, #174424, #185329, #78298, #161480, #192565, #66277, #110158, #84674, #130779, #113912, #240350 ) ) ;
#97072=VECTOR ( 'NONE', #251228, 1000.000000000000000 ) ;
#97242=EDGE_LOOP ( 'NONE', ( #141581, #195053, #7117, #241628, #105125, #35287, #211126, #130950, #10212, #100515 ) ) ;
#97322=DIRECTION ( 'NONE',  ( 1.186688945009010077E-16, 0.9651348961777157509, -0.2617529984165031243 ) ) ;
#97392=ORIENTED_EDGE ( 'NONE', *, *, #170186, .T. ) ;
#97609=CARTESIAN_POINT ( 'NONE',  ( -23.25000000000000355, 65.08943781962308606, -222.1672656287770451 ) ) ;
#97869=DIRECTION ( 'NONE',  ( 1.000000000000000000, 0.000000000000000000, 0.000000000000000000 ) ) ;
#98129=( BOUNDED_CURVE ( )  B_SPLINE_CURVE ( 3, ( #167189, #246678, #121631, #165891 ),
 .UNSPECIFIED., .F., .F. ) 
 B_SPLINE_CURVE_WITH_KNOTS ( ( 4, 4 ),
 ( 4.712388980384681680, 5.672655318024688142 ),
 .UNSPECIFIED. ) 
 CURVE ( )  GEOMETRIC_REPRESENTATION_ITEM ( )  RATIONAL_B_SPLINE_CURVE ( ( 1.000000000000000000, 0.9246222802177346267, 0.9246222802177346267, 1.000000000000000000 ) ) 
 REPRESENTATION_ITEM ( '' )  );
#98146=ORIENTED_EDGE ( 'NONE', *, *, #209856, .T. ) ;
#98148=CARTESIAN_POINT ( 'NONE',  ( 16.27683809663750125, 60.62847850914943137, -224.4802381816402033 ) ) ;
#98225=EDGE_LOOP ( 'NONE', ( #117524, #167219, #63900, #78613, #45554, #59273, #10585, #1636, #12602 ) ) ;
#98261=ADVANCED_FACE ( 'NONE', ( #169218 ), #111782, .F. ) ;
#98336=LINE ( 'NONE', #120541, #58231 ) ;
#98710=ORIENTED_EDGE ( 'NONE', *, *, #232770, .F. ) ;
#98739=CARTESIAN_POINT ( 'NONE',  ( -18.40000000000000213, 59.20211495293902004, -220.5705723384363921 ) ) ;
#98771=ORIENTED_EDGE ( 'NONE', *, *, #145328, .T. ) ;
#98781=EDGE_CURVE ( 'NONE', #257876, #146129, #192296, .T. ) ;
#99137=CARTESIAN_POINT ( 'NONE',  ( 23.04999999999999716, 61.13752757784637026, -224.6182967272386009 ) ) ;
#99188=CARTESIAN_POINT ( 'NONE',  ( 20.99999999999999645, 61.13238474529445909, -221.0940783352693586 ) ) ;
#99355=CARTESIAN_POINT ( 'NONE',  ( -16.94445028196808778, 60.88759175473954599, -221.0718995934454938 ) ) ;
#99363=ORIENTED_EDGE ( 'NONE', *, *, #210018, .T. ) ;
#99374=LINE ( 'NONE', #117678, #219983 ) ;
#99390=VECTOR ( 'NONE', #220502, 1000.000000000000000 ) ;
#99426=AXIS2_PLACEMENT_3D ( 'NONE', #162933, #242434, #80779 ) ;
#99629=CARTESIAN_POINT ( 'NONE',  ( -16.91776028072577631, 63.07934927644033252, -213.0999624438847775 ) ) ;
#99697=ORIENTED_EDGE ( 'NONE', *, *, #153853, .F. ) ;
#99820=CARTESIAN_POINT ( 'NONE',  ( -16.97683809663752186, 60.04939757144280321, -224.3231863825903076 ) ) ;
#99893=DIRECTION ( 'NONE',  ( -1.073024830501117725E-15, -0.2617529984165031243, -0.9651348961777157509 ) ) ;
#99897=LINE ( 'NONE', #219875, #18442 ) ;
#99952=VERTEX_POINT ( 'NONE', #175364 ) ;
#99957=DIRECTION ( 'NONE',  ( 1.000000000000000000, 0.000000000000000000, 0.000000000000000000 ) ) ;
#100222=DIRECTION ( 'NONE',  ( 1.186688945009010077E-16, 0.9651348961777157509, -0.2617529984165031243 ) ) ;
#100347=LINE ( 'NONE', #80785, #169104 ) ;
#100410=CARTESIAN_POINT ( 'NONE',  ( -16.87786941232801041, 63.08497791849498526, -213.0992491019884483 ) ) ;
#100443=AXIS2_PLACEMENT_3D ( 'NONE', #160326, #123746, #62492 ) ;
#100504=EDGE_LOOP ( 'NONE', ( #26639, #202217, #61256, #200880 ) ) ;
#100515=ORIENTED_EDGE ( 'NONE', *, *, #138189, .T. ) ;
#100526=CARTESIAN_POINT ( 'NONE',  ( -16.90138253750127362, 63.04949597677561712, -213.2612322484624485 ) ) ;
#100657=ORIENTED_EDGE ( 'NONE', *, *, #178243, .F. ) ;
#101052=CARTESIAN_POINT ( 'NONE',  ( -16.87683809663752399, 61.23280479334025017, -220.3417702668379832 ) ) ;
#101158=CARTESIAN_POINT ( 'NONE',  ( 23.04999999999999716, 64.17386235947780904, -213.4227319315771183 ) ) ;
#101233=CARTESIAN_POINT ( 'NONE',  ( -17.01825945287482966, 60.84284427644114146, -221.0155524357444108 ) ) ;
#101238=CARTESIAN_POINT ( 'NONE',  ( -16.94878442675511110, 63.05546222811283030, -213.0798118229344595 ) ) ;
#101248=ORIENTED_EDGE ( 'NONE', *, *, #218391, .F. ) ;
#101306=CARTESIAN_POINT ( 'NONE',  ( -18.40000000000000213, 62.49259387941005173, -209.4439336506227960 ) ) ;
#101925=CARTESIAN_POINT ( 'NONE',  ( 13.88638282980483041, 62.94602368561173478, -215.5245807872942407 ) ) ;
#102030=VERTEX_POINT ( 'NONE', #15421 ) ;
#102157=EDGE_CURVE ( 'NONE', #51883, #77430, #141752, .T. ) ;
#102186=CARTESIAN_POINT ( 'NONE',  ( -17.27223548805033460, 63.04010829898014379, -211.7852720176618675 ) ) ;
#102225=CARTESIAN_POINT ( 'NONE',  ( -17.04295772865306446, 63.01344430405035268, -213.1080164377868300 ) ) ;
#102337=AXIS2_PLACEMENT_3D ( 'NONE', #208121, #46444, #7327 ) ;
#102377=ORIENTED_EDGE ( 'NONE', *, *, #236833, .F. ) ;
#102480=( LENGTH_UNIT ( ) NAMED_UNIT ( * ) SI_UNIT ( .MILLI., .METRE. ) );
#102536=CARTESIAN_POINT ( 'NONE',  ( -16.87036670365548474, 63.08160062417908165, -212.9922606024214531 ) ) ;
#102804=ORIENTED_EDGE ( 'NONE', *, *, #13309, .F. ) ;
#102903=LINE ( 'NONE', #145892, #112917 ) ;
#103005=CARTESIAN_POINT ( 'NONE',  ( 20.99999999999999645, 60.24242455067834356, -224.3755369822736156 ) ) ;
#103304=EDGE_CURVE ( 'NONE', #50473, #67123, #169792, .T. ) ;
#103635=CARTESIAN_POINT ( 'NONE',  ( -16.97683809663752186, 61.13629130372252973, -220.3155949669961444 ) ) ;
#103709=CARTESIAN_POINT ( 'NONE',  ( -16.86337532320261801, 60.88454159514807174, -221.1293591871273350 ) ) ;
#103770=SURFACE_STYLE_USAGE ( .BOTH. , #24287 ) ;
#103916=CARTESIAN_POINT ( 'NONE',  ( -16.77180007708459186, 60.93559221856046548, -221.0556120513950873 ) ) ;
#103977=CIRCLE ( 'NONE', #37383, 0.1000000000000035305 ) ;
#104050=CARTESIAN_POINT ( 'NONE',  ( -16.88815647973233780, 60.93782573408322634, -221.0441957042815773 ) ) ;
#104146=CARTESIAN_POINT ( 'NONE',  ( -33.72168855820452649, 48.78215419113038109, -213.4964773079645681 ) ) ;
#104178=CARTESIAN_POINT ( 'NONE',  ( -12.25000000000000178, 62.10905854918435409, -217.1108499610990918 ) ) ;
#104464=CARTESIAN_POINT ( 'NONE',  ( -21.64999999999999858, 60.62847850914943848, -224.4802381816402317 ) ) ;
#104526=CARTESIAN_POINT ( 'NONE',  ( 14.77516762759922386, 62.09620004573545771, -218.7373296619003327 ) ) ;
#104937=CARTESIAN_POINT ( 'NONE',  ( -14.00000000000000178, 62.10905854918435409, -217.1108499610990918 ) ) ;
#105034=SHAPE_REPRESENTATION_RELATIONSHIP ( 'NONE' , 'NONE' ,  #198303, #51500 ) ;
#105125=ORIENTED_EDGE ( 'NONE', *, *, #58822, .T. ) ;
#105258=CARTESIAN_POINT ( 'NONE',  ( -12.48127053791144547, 62.79551507739392235, -216.3883973845401840 ) ) ;
#105296=LINE ( 'NONE', #182324, #29311 ) ;
#105416=FILL_AREA_STYLE_COLOUR ( '', #56367 ) ;
#105533=EDGE_CURVE ( 'NONE', #179633, #58353, #245475, .T. ) ;
#105646=CARTESIAN_POINT ( 'NONE',  ( -12.25000000000000711, 62.53104822794669815, -217.4650886355768762 ) ) ;
#105776=CARTESIAN_POINT ( 'NONE',  ( 15.57250062127602419, 62.77489950700472576, -216.4869172218852214 ) ) ;
#105821=DIRECTION ( 'NONE',  ( -0.000000000000000000, 0.2617529984165031243, 0.9651348961777157509 ) ) ;
#105924=DIRECTION ( 'NONE',  ( 0.000000000000000000, -0.2617529984165031243, -0.9651348961777157509 ) ) ;
#105959=EDGE_CURVE ( 'NONE', #253697, #66070, #64325, .T. ) ;
#106154=CARTESIAN_POINT ( 'NONE',  ( -21.64999999999999858, 61.51843870376554690, -221.1987795346359746 ) ) ;
#106319=DIRECTION ( 'NONE',  ( 0.000000000000000000, 0.2617529984164506107, 0.9651348961777299618 ) ) ;
#106470=FACE_OUTER_BOUND ( 'NONE', #124206, .T. ) ;
#106481=ORIENTED_EDGE ( 'NONE', *, *, #232902, .F. ) ;
#106558=PLANE ( 'NONE',  #73756 ) ;
#106562=CARTESIAN_POINT ( 'NONE',  ( -15.75000000000001421, 62.62153588618861733, -217.1314428046943874 ) ) ;
#106581=ORIENTED_EDGE ( 'NONE', *, *, #134452, .T. ) ;
#106649=DIRECTION ( 'NONE',  ( -1.000000000000000000, -0.000000000000000000, 0.000000000000000000 ) ) ;
#106722=PRESENTATION_STYLE_ASSIGNMENT (( #6341 ) ) ;
#106878=CARTESIAN_POINT ( 'NONE',  ( 23.24999999999999645, 61.34848953995434329, -212.6564661897791382 ) ) ;
#106918=ORIENTED_EDGE ( 'NONE', *, *, #225965, .F. ) ;
#106944=CARTESIAN_POINT ( 'NONE',  ( -13.54795643572458808, 62.05093865251257768, -218.8507522889722452 ) ) ;
#106978=EDGE_LOOP ( 'NONE', ( #205723, #133577, #72384, #437 ) ) ;
#107053=ADVANCED_FACE ( 'NONE', ( #247160 ), #9845, .F. ) ;
#107089=ORIENTED_EDGE ( 'NONE', *, *, #198656, .F. ) ;
#107120=CARTESIAN_POINT ( 'NONE',  ( 15.75000000000000000, 62.53104822794671236, -217.4650886355768478 ) ) ;
#107781=CARTESIAN_POINT ( 'NONE',  ( -18.40000000000000213, 62.48575673152180343, -209.5207689439494345 ) ) ;
#107964=CARTESIAN_POINT ( 'NONE',  ( -16.77828822459933633, 63.08606603224484388, -213.1407965249532310 ) ) ;
#107970=AXIS2_PLACEMENT_3D ( 'NONE', #205766, #106649, #186220 ) ;
#107985=VERTEX_POINT ( 'NONE', #182058 ) ;
#108072=AXIS2_PLACEMENT_3D ( 'NONE', #59813, #100222, #196773 ) ;
#108090=ORIENTED_EDGE ( 'NONE', *, *, #45816, .F. ) ;
#108428=DIRECTION ( 'NONE',  ( -0.000000000000000000, 0.2617529984165031243, 0.9651348961777157509 ) ) ;
#108565=CARTESIAN_POINT ( 'NONE',  ( -16.27683809663750480, 63.69098859062252416, -213.1881598963609576 ) ) ;
#108616=CARTESIAN_POINT ( 'NONE',  ( 23.24999999999999645, 61.13752757784637026, -224.6182967272386009 ) ) ;
#108741=DIRECTION ( 'NONE',  ( -1.000000000000000000, -0.000000000000000000, 0.000000000000000000 ) ) ;
#108855=VECTOR ( 'NONE', #212799, 1000.000000000000000 ) ;
#108970=EDGE_CURVE ( 'NONE', #6716, #25976, #252994, .T. ) ;
#109052=LINE ( 'NONE', #247276, #96122 ) ;
#109137=CARTESIAN_POINT ( 'NONE',  ( -15.15564720441981805, 62.87834062276081681, -215.9526216959265810 ) ) ;
#109201=DIRECTION ( 'NONE',  ( -1.073024830501117725E-15, 0.2617529984165031243, 0.9651348961777157509 ) ) ;
#109558=DIRECTION ( 'NONE',  ( 1.000000000000000000, 0.000000000000000000, 0.000000000000000000 ) ) ;
#109845=ORIENTED_EDGE ( 'NONE', *, *, #33141, .T. ) ;
#110158=ORIENTED_EDGE ( 'NONE', *, *, #14714, .F. ) ;
#110195=VERTEX_POINT ( 'NONE', #104178 ) ;
#110713=ORIENTED_EDGE ( 'NONE', *, *, #228054, .T. ) ;
#110798=ORIENTED_EDGE ( 'NONE', *, *, #2422, .F. ) ;
#110804=CARTESIAN_POINT ( 'NONE',  ( -14.56556274378147009, 62.06390979127200325, -218.8186321886648784 ) ) ;
#111209=LINE ( 'NONE', #72094, #213826 ) ;
#111728=ADVANCED_FACE ( 'NONE', ( #144494 ), #126227, .T. ) ;
#111731=AXIS2_PLACEMENT_3D ( 'NONE', #246594, #92659, #10575 ) ;
#111782=PLANE ( 'NONE',  #192784 ) ;
#111789=CARTESIAN_POINT ( 'NONE',  ( -16.93658623642897609, 60.90006327965645028, -221.0705442474995266 ) ) ;
#111892=CARTESIAN_POINT ( 'NONE',  ( -15.75000000000000355, 62.10905854918435409, -217.1108499610990918 ) ) ;
#112017=CARTESIAN_POINT ( 'NONE',  ( -16.91049119928363353, 60.93105485803026511, -221.0723421939750324 ) ) ;
#112081=VECTOR ( 'NONE', #152547, 1000.000000000000000 ) ;
#112245=CARTESIAN_POINT ( 'NONE',  ( 12.68104795156994591, 62.84928511903725479, -216.1139082291015256 ) ) ;
#112272=CARTESIAN_POINT ( 'NONE',  ( -21.65000000000000213, 63.54522198573874192, -221.7484608313106378 ) ) ;
#112675=LINE ( 'NONE', #149249, #135390 ) ;
#112746=CARTESIAN_POINT ( 'NONE',  ( -16.89268316805465986, 63.08557629953710943, -213.1216189793661329 ) ) ;
#112831=CARTESIAN_POINT ( 'NONE',  ( -18.40000000000000213, 61.13752757784637026, -224.6182967272386009 ) ) ;
#112917=VECTOR ( 'NONE', #182487, 1000.000000000000000 ) ;
#113058=ORIENTED_EDGE ( 'NONE', *, *, #102157, .T. ) ;
#113316=ORIENTED_EDGE ( 'NONE', *, *, #70557, .T. ) ;
#113347=ORIENTED_EDGE ( 'NONE', *, *, #17791, .F. ) ;
#113479=LINE ( 'NONE', #195616, #31557 ) ;
#113553=ORIENTED_EDGE ( 'NONE', *, *, #118413, .F. ) ;
#113762=ORIENTED_EDGE ( 'NONE', *, *, #102157, .F. ) ;
#113912=ORIENTED_EDGE ( 'NONE', *, *, #148157, .F. ) ;
#114133=CARTESIAN_POINT ( 'NONE',  ( -18.40000000000000213, 62.48575673152180343, -209.5207689439494345 ) ) ;
#114440=FACE_OUTER_BOUND ( 'NONE', #89833, .T. ) ;
#114568=AXIS2_PLACEMENT_3D ( 'NONE', #240931, #183523, #144355 ) ;
#114846=ORIENTED_EDGE ( 'NONE', *, *, #145328, .F. ) ;
#115091=CARTESIAN_POINT ( 'NONE',  ( -16.84793658983424436, 63.06383758434998299, -213.2083519146329422 ) ) ;
#115316=DIRECTION ( 'NONE',  ( 0.000000000000000000, -0.9651348961777155289, 0.2617529984165037904 ) ) ;
#115490=CARTESIAN_POINT ( 'NONE',  ( -16.87036670365549895, 60.86740053880574663, -221.1564527318009254 ) ) ;
#115631=CARTESIAN_POINT ( 'NONE',  ( -16.94275863009466576, 60.89032433645830622, -221.0716331249102495 ) ) ;
#115655=CARTESIAN_POINT ( 'NONE',  ( -18.34374000495059676, 62.50563584222673796, -209.4474707446456421 ) ) ;
#115799=PRODUCT_DEFINITION_CONTEXT ( 'detailed design', #37539, 'design' ) ;
#115941=VERTEX_POINT ( 'NONE', #168212 ) ;
#116061=VERTEX_POINT ( 'NONE', #233300 ) ;
#116432=CARTESIAN_POINT ( 'NONE',  ( -17.01473183483381035, 60.96553306590055854, -220.9452142459682875 ) ) ;
#116453=EDGE_CURVE ( 'NONE', #127095, #205367, #253794, .T. ) ;
#116562=EDGE_CURVE ( 'NONE', #174664, #205367, #240667, .T. ) ;
#116568=EDGE_CURVE ( 'NONE', #174664, #238512, #217230, .T. ) ;
#116655=CARTESIAN_POINT ( 'NONE',  ( -16.94275863006528482, 63.05852775302872715, -213.0770397792431083 ) ) ;
#116755=ORIENTED_EDGE ( 'NONE', *, *, #31353, .F. ) ;
#116833=VECTOR ( 'NONE', #18878, 1000.000000000000000 ) ;
#116913=CARTESIAN_POINT ( 'NONE',  ( -16.90257928357875272, 60.93180429990802338, -221.0538891728311057 ) ) ;
#116959=LINE ( 'NONE', #195242, #242575 ) ;
#116966=CARTESIAN_POINT ( 'NONE',  ( -16.97683809663752186, 61.13629130372252973, -220.3155949669961444 ) ) ;
#117273=CARTESIAN_POINT ( 'NONE',  ( -16.79184697841823848, 60.94163718135611418, -221.0380540244521228 ) ) ;
#117335=B_SPLINE_CURVE_WITH_KNOTS ( 'NONE', 3,
 ( #199565, #78290, #100410, #155309, #56154, #17071, #96560, #77013, #156600, #236091 ),
 .UNSPECIFIED., .F., .F.,
 ( 4, 3, 3, 4 ),
 ( 7.632826238677508298E-06, 4.756916949875313879E-05, 9.484459048148540536E-05, 0.0001435500935099941200 ),
 .UNSPECIFIED. ) ;
#117409=CARTESIAN_POINT ( 'NONE',  ( -16.87683809663752399, 50.04486772930183491, -218.0870470535037100 ) ) ;
#117524=ORIENTED_EDGE ( 'NONE', *, *, #254698, .T. ) ;
#117579=CARTESIAN_POINT ( 'NONE',  ( 20.27550659511089037, 63.79409916874961795, -213.3197368432687426 ) ) ;
#117610=ORIENTED_EDGE ( 'NONE', *, *, #219697, .F. ) ;
#117678=CARTESIAN_POINT ( 'NONE',  ( -20.65000000000000568, 63.54522198573874192, -221.7484608313106378 ) ) ;
#117688=EDGE_LOOP ( 'NONE', ( #147026, #101248, #176432, #158415 ) ) ;
#117835=ORIENTED_EDGE ( 'NONE', *, *, #149767, .F. ) ;
#118062=CARTESIAN_POINT ( 'NONE',  ( -16.94107738177415712, 60.85118289042637940, -221.1214263997032106 ) ) ;
#118172=AXIS2_PLACEMENT_3D ( 'NONE', #93093, #153124, #134770 ) ;
#118381=CARTESIAN_POINT ( 'NONE',  ( -18.40000000000000213, 61.34848953995435039, -212.6564661897791098 ) ) ;
#118388=CARTESIAN_POINT ( 'NONE',  ( -16.97683810757273193, 61.09996331030407646, -220.4495434389081367 ) ) ;
#118413=EDGE_CURVE ( 'NONE', #10339, #39830, #140593, .T. ) ;
#118419=ORIENTED_EDGE ( 'NONE', *, *, #161274, .F. ) ;
#118476=VERTEX_POINT ( 'NONE', #211858 ) ;
#118743=DIRECTION ( 'NONE',  ( -1.000000000000000000, 0.000000000000000000, 0.000000000000000000 ) ) ;
#118873=VERTEX_POINT ( 'NONE', #117579 ) ;
#118956=CARTESIAN_POINT ( 'NONE',  ( -16.77308656112214891, 63.08568178456688713, -213.1278080429823092 ) ) ;
#119105=DIRECTION ( 'NONE',  ( -0.000000000000000000, 0.2617529984165031243, 0.9651348961777157509 ) ) ;
#119201=B_SPLINE_CURVE_WITH_KNOTS ( 'NONE', 3,
 ( #214460, #158390, #257387, #116655, #60516, #80055, #201328, #177931, #196194, #99629, #236588, #78789, #76232 ),
 .UNSPECIFIED., .F., .F.,
 ( 4, 3, 3, 3, 4 ),
 ( -3.224855718259041645E-06, 0.000000000000000000, 6.199515528676308480E-06, 4.034952380128061856E-05, 7.452715123701166987E-05 ),
 .UNSPECIFIED. ) ;
#119370=DIRECTION ( 'NONE',  ( 1.000000000000000000, -2.808674667590276147E-16, -1.035613708381807261E-15 ) ) ;
#119505=LINE ( 'NONE', #19101, #79089 ) ;
#119541=DIRECTION ( 'NONE',  ( 0.000000000000000000, -0.9651348961777157509, 0.2617529984165031243 ) ) ;
#119690=CARTESIAN_POINT ( 'NONE',  ( 17.74533788810830259, 59.48958453972256422, -223.0693145980908980 ) ) ;
#119884=CARTESIAN_POINT ( 'NONE',  ( -17.11825945287481332, 63.05955705323258798, -213.2241350765465882 ) ) ;
#119910=ADVANCED_FACE ( 'NONE', ( #68553 ), #148088, .F. ) ;
#119911=( BOUNDED_CURVE ( )  B_SPLINE_CURVE ( 3, ( #45150, #6012, #67284, #244628 ),
 .UNSPECIFIED., .F., .F. ) 
 B_SPLINE_CURVE_WITH_KNOTS ( ( 4, 4 ),
 ( 1.570796326794908992, 2.617993877991592555 ),
 .UNSPECIFIED. ) 
 CURVE ( )  GEOMETRIC_REPRESENTATION_ITEM ( )  RATIONAL_B_SPLINE_CURVE ( ( 1.000000000000000000, 0.9106836025229446685, 0.9106836025229446685, 1.000000000000000000 ) ) 
 REPRESENTATION_ITEM ( '' )  );
#120162=AXIS2_PLACEMENT_3D ( 'NONE', #181554, #45872, #201095 ) ;
#120265=CARTESIAN_POINT ( 'NONE',  ( -16.80891096016324227, 63.09035564583723499, -213.1105745952694690 ) ) ;
#120272=VECTOR ( 'NONE', #147263, 1000.000000000000000 ) ;
#120328=LINE ( 'NONE', #77291, #59015 ) ;
#120347=( BOUNDED_CURVE ( )  B_SPLINE_CURVE ( 3, ( #114133, #249809, #50300, #69909 ),
 .UNSPECIFIED., .F., .T. ) 
 B_SPLINE_CURVE_WITH_KNOTS ( ( 4, 4 ),
 ( 5.733388419619900311, 5.983100554402347449 ),
 .UNSPECIFIED. ) 
 CURVE ( )  GEOMETRIC_REPRESENTATION_ITEM ( )  RATIONAL_B_SPLINE_CURVE ( ( 1.000000000000000000, 0.9948104011409416580, 0.9948104011409416580, 1.000000000000000000 ) ) 
 REPRESENTATION_ITEM ( '' )  );
#120504=EDGE_CURVE ( 'NONE', #231042, #74054, #122463, .T. ) ;
#120533=CARTESIAN_POINT ( 'NONE',  ( -18.41431012584568094, 62.49790673650496586, -209.4212991392053311 ) ) ;
#120541=CARTESIAN_POINT ( 'NONE',  ( -33.72168855820451938, 63.08573235307422777, -213.1276215869287398 ) ) ;
#120660=CARTESIAN_POINT ( 'NONE',  ( -16.92570016628984675, 60.92319296112430749, -221.0677532620695160 ) ) ;
#120864=CARTESIAN_POINT ( 'NONE',  ( -16.93255653858138388, 60.87470302366463670, -221.0950187931682649 ) ) ;
#120909=ADVANCED_FACE ( 'NONE', ( #158734 ), #78328, .T. ) ;
#120970=CARTESIAN_POINT ( 'NONE',  ( -16.79270642812307557, 60.94587935087318442, -221.0320299440186318 ) ) ;
#121009=PLANE ( 'NONE',  #114568 ) ;
#121290=VECTOR ( 'NONE', #251852, 1000.000000000000000 ) ;
#121631=CARTESIAN_POINT ( 'NONE',  ( -16.98495255085919098, 60.88170416505755611, -221.0420300672591623 ) ) ;
#121804=CARTESIAN_POINT ( 'NONE',  ( -17.80356949363990182, 62.80985299201304173, -210.6043626271361973 ) ) ;
#122064=PLANE ( 'NONE',  #169979 ) ;
#122148=CARTESIAN_POINT ( 'NONE',  ( -16.90202395485715314, 63.08422021722274309, -213.0722826622215678 ) ) ;
#122151=CARTESIAN_POINT ( 'NONE',  ( -21.65000000000000213, 62.98921886345645760, -213.1014462870871569 ) ) ;
#122439=LINE ( 'NONE', #143271, #137713 ) ;
#122463=LINE ( 'NONE', #41655, #242391 ) ;
#122774=AXIS2_PLACEMENT_3D ( 'NONE', #216176, #58368, #37571 ) ;
#123436=CIRCLE ( 'NONE', #77605, 0.9000000000000014655 ) ;
#123513=CARTESIAN_POINT ( 'NONE',  ( -16.88705144915410017, 61.01290475571573779, -220.7705454887500593 ) ) ;
#123516=CARTESIAN_POINT ( 'NONE',  ( -18.40000000000000213, 65.08943781962308606, -222.1672656287770451 ) ) ;
#123586=CARTESIAN_POINT ( 'NONE',  ( -15.57281606413133979, 62.77476515014583924, -216.4875458411299860 ) ) ;
#123653=CARTESIAN_POINT ( 'NONE',  ( -16.87383368123029825, 60.93935776605891164, -221.0417277355860790 ) ) ;
#123746=DIRECTION ( 'NONE',  ( 0.000000000000000000, 0.9651348961777157509, -0.2617529984165031243 ) ) ;
#123900=CARTESIAN_POINT ( 'NONE',  ( -14.00000000000000178, 62.10905854918435409, -217.1108499610990918 ) ) ;
#124122=VERTEX_POINT ( 'NONE', #166585 ) ;
#124206=EDGE_LOOP ( 'NONE', ( #222928, #83463, #84470, #231257 ) ) ;
#124331=CARTESIAN_POINT ( 'NONE',  ( -21.64999999999999858, 62.98921886345645760, -213.1014462870871569 ) ) ;
#124335=VECTOR ( 'NONE', #53772, 1000.000000000000000 ) ;
#124413=CARTESIAN_POINT ( 'NONE',  ( -16.91049119928362998, 63.09403526110288141, -213.0970071285398433 ) ) ;
#124642=ORIENTED_EDGE ( 'NONE', *, *, #190262, .T. ) ;
#124657=SURFACE_STYLE_FILL_AREA ( #243295 ) ;
#124776=VECTOR ( 'NONE', #208308, 1000.000000000000000 ) ;
#124871=CARTESIAN_POINT ( 'NONE',  ( -14.45422546970484312, 62.93791375105570296, -215.5805554555300318 ) ) ;
#125077=EDGE_LOOP ( 'NONE', ( #107089, #173982, #72505 ) ) ;
#125325=EDGE_CURVE ( 'NONE', #136892, #243144, #41235, .T. ) ;
#125436=CARTESIAN_POINT ( 'NONE',  ( 18.54999999999999716, 60.93935776605888321, -221.0417277355861359 ) ) ;
#125672=EDGE_CURVE ( 'NONE', #249995, #236891, #178648, .T. ) ;
#125836=ORIENTED_EDGE ( 'NONE', *, *, #54667, .F. ) ;
#126041=DIRECTION ( 'NONE',  ( 0.000000000000000000, -0.9651348961777157509, 0.2617529984165031243 ) ) ;
#126227=CYLINDRICAL_SURFACE ( 'NONE', #107970, 0.1000000000000124678 ) ;
#126371=EDGE_CURVE ( 'NONE', #87486, #24894, #84064, .T. ) ;
#126525=CARTESIAN_POINT ( 'NONE',  ( -13.77178122865954535, 62.03415779510192607, -218.8921516991029534 ) ) ;
#126653=CARTESIAN_POINT ( 'NONE',  ( 13.77030915526557386, 62.94440715787351337, -215.5359628679902357 ) ) ;
#127011=CIRCLE ( 'NONE', #193653, 0.9000000000000014655 ) ;
#127095=VERTEX_POINT ( 'NONE', #118381 ) ;
#127240=DIRECTION ( 'NONE',  ( 0.000000000000000000, -0.2617529984165031243, -0.9651348961777157509 ) ) ;
#127528=ORIENTED_EDGE ( 'NONE', *, *, #174616, .T. ) ;
#127671=DIRECTION ( 'NONE',  ( 1.186688945009009831E-16, 0.9651348961777157509, -0.2617529984165031243 ) ) ;
#127817=CARTESIAN_POINT ( 'NONE',  ( -13.43673303185029511, 62.06361769656464134, -218.8193597571736575 ) ) ;
#127894=CIRCLE ( 'NONE', #86159, 0.1000000000000106498 ) ;
#127961=VECTOR ( 'NONE', #32665, 999.9999999999998863 ) ;
#128437=CARTESIAN_POINT ( 'NONE',  ( -17.80356949364355401, 59.42639550586179098, -223.0798372515704102 ) ) ;
#128564=FACE_OUTER_BOUND ( 'NONE', #221322, .T. ) ;
#128579=( BOUNDED_SURFACE ( )  B_SPLINE_SURFACE ( 3, 2, ( 
 ( #17288, #175115, #75967 ),
 ( #178955, #219315, #236315 ),
 ( #138474, #60239, #139763 ),
 ( #214197, #194659, #218016 ),
 ( #19857, #35583, #96774 ),
 ( #39438, #56378, #176373 ),
 ( #255833, #115091, #155537 ),
 ( #233767, #235047, #40726 ),
 ( #38138, #78515, #120265 ),
 ( #16016, #118956, #197185 ) ),
 .UNSPECIFIED., .F., .F., .F. ) 
 B_SPLINE_SURFACE_WITH_KNOTS ( ( 4, 2, 2, 2, 4 ),
 ( 3, 3 ),
 ( 0.002161241639767263849, 0.002579950749615834808, 0.002789305304540120288, 0.002893982582002263028, 0.002998659859464405768 ),
 ( 0.000000000000000000, 1.000000000000000000 ),
 .UNSPECIFIED. ) 
 GEOMETRIC_REPRESENTATION_ITEM ( )  RATIONAL_B_SPLINE_SURFACE ( (
 ( 1.000000000000000000, 0.7071067811865475727, 1.000000000000000000),
 ( 1.000000000000000000, 0.7632447400659811976, 1.000000000000000000),
 ( 1.000000000000000000, 0.8158073005116185383, 1.000000000000000000),
 ( 1.000000000000000000, 0.8906973462392635543, 1.000000000000000000),
 ( 1.000000000000000000, 0.9149408947804374970, 1.000000000000000000),
 ( 1.000000000000000000, 0.9493368785273612609, 1.000000000000000000),
 ( 1.000000000000000000, 0.9605194247158702625, 1.000000000000000000),
 ( 1.000000000000000000, 0.9803630264779076287, 1.000000000000000000),
 ( 1.000000000000000000, 0.9900844824272719835, 1.000000000000000000),
 ( 1.000000000000000000, 0.9894588281429380627, 1.000000000000000000) ) ) 
 REPRESENTATION_ITEM ( '' )  SURFACE ( )  );
#128617=DIRECTION ( 'NONE',  ( -1.000000000000000000, -0.000000000000000000, -0.000000000000000000 ) ) ;
#128618=FACE_OUTER_BOUND ( 'NONE', #77094, .T. ) ;
#128697=DIRECTION ( 'NONE',  ( 0.7071067811865493491, -0.6824534298470356086, 0.1850873201762205378 ) ) ;
#128809=LINE ( 'NONE', #188764, #172102 ) ;
#129001=CARTESIAN_POINT ( 'NONE',  ( 20.99999999999999645, 63.27875933230978234, -213.1799721866121047 ) ) ;
#129149=EDGE_CURVE ( 'NONE', #166275, #21828, #249336, .T. ) ;
#129385=ORIENTED_EDGE ( 'NONE', *, *, #171046, .F. ) ;
#129683=CARTESIAN_POINT ( 'NONE',  ( -16.87036670365548474, 63.08160062417908165, -212.9922606024214531 ) ) ;
#129692=CARTESIAN_POINT ( 'NONE',  ( -15.55912972643741199, 62.32143948325225580, -221.5201728061774986 ) ) ;
#129736=CARTESIAN_POINT ( 'NONE',  ( -16.89081410710458542, 63.08561305663506857, -213.1230241508039853 ) ) ;
#129803=CARTESIAN_POINT ( 'NONE',  ( -16.83794237512074332, 61.00236442716369822, -220.8997268849512920 ) ) ;
#129977=ORIENTED_EDGE ( 'NONE', *, *, #241537, .T. ) ;
#130423=ORIENTED_EDGE ( 'NONE', *, *, #74848, .F. ) ;
#130599=PRODUCT ( 'Snap Open Cable Crossbars 10', 'Snap Open Cable Crossbars 10', '', ( #90053 ) ) ;
#130779=ORIENTED_EDGE ( 'NONE', *, *, #103304, .F. ) ;
#130884=ADVANCED_FACE ( 'NONE', ( #158976 ), #42849, .F. ) ;
#130950=ORIENTED_EDGE ( 'NONE', *, *, #145008, .T. ) ;
#131017=CARTESIAN_POINT ( 'NONE',  ( -16.87331047859649757, 63.08573235307424198, -213.1276215869287967 ) ) ;
#131142=DIRECTION ( 'NONE',  ( -1.000000000000000000, -2.808674667590276147E-16, -1.035613708381807261E-15 ) ) ;
#131201=CARTESIAN_POINT ( 'NONE',  ( -18.39999999999999858, 58.58048437606812087, -223.8992190685246157 ) ) ;
#131235=EDGE_LOOP ( 'NONE', ( #206156, #192786, #185590 ) ) ;
#131338=CARTESIAN_POINT ( 'NONE',  ( -16.92132318717937522, 60.91662537786660181, -221.0641526825682490 ) ) ;
#131371=CIRCLE ( 'NONE', #143831, 14.30833333333334245 ) ;
#131395=MECHANICAL_DESIGN_GEOMETRIC_PRESENTATION_REPRESENTATION('',(#85560),#164720);
#131420=COLOUR_RGB ( '', 0.40784314, 0.44705882, 0.49803922) ;
#131433=ADVANCED_FACE ( 'NONE', ( #134565 ), #177603, .F. ) ;
#131447=FACE_OUTER_BOUND ( 'NONE', #163999, .T. ) ;
#131519=EDGE_LOOP ( 'NONE', ( #75347, #181184, #68741, #225210, #44091, #125836, #114846, #106481, #235184, #99697, #22263, #74056, #23344, #75304 ) ) ;
#131560=ADVANCED_FACE ( 'NONE', ( #203554 ), #39377, .F. ) ;
#131600=ORIENTED_EDGE ( 'NONE', *, *, #17791, .T. ) ;
#131632=DIRECTION ( 'NONE',  ( 0.000000000000000000, 0.2617529984165031243, 0.9651348961777157509 ) ) ;
#131710=ORIENTED_EDGE ( 'NONE', *, *, #120504, .T. ) ;
#131946=ORIENTED_EDGE ( 'NONE', *, *, #125325, .T. ) ;
#132298=CARTESIAN_POINT ( 'NONE',  ( -16.88853107394619357, 63.08565309574376556, -213.1245576704256735 ) ) ;
#132383=ORIENTED_EDGE ( 'NONE', *, *, #31353, .T. ) ;
#132799=ORIENTED_EDGE ( 'NONE', *, *, #179217, .F. ) ;
#133081=CARTESIAN_POINT ( 'NONE',  ( 12.60873083341397916, 62.83289218956782207, -216.2009511582251378 ) ) ;
#133225=VERTEX_POINT ( 'NONE', #248940 ) ;
#133396=CARTESIAN_POINT ( 'NONE',  ( -15.39946565075089779, 62.27203542310181206, -218.2690822304508629 ) ) ;
#133577=ORIENTED_EDGE ( 'NONE', *, *, #186956, .F. ) ;
#133708=LINE ( 'NONE', #75059, #34200 ) ;
#134058=EDGE_CURVE ( 'NONE', #75872, #99952, #233575, .T. ) ;
#134267=CARTESIAN_POINT ( 'NONE',  ( -16.87331047859649757, 63.08573235307424198, -213.1276215869287967 ) ) ;
#134436=CARTESIAN_POINT ( 'NONE',  ( -21.65000000000000213, 60.96553306590055854, -220.9452142459683159 ) ) ;
#134452=EDGE_CURVE ( 'NONE', #83517, #118873, #153773, .T. ) ;
#134565=FACE_OUTER_BOUND ( 'NONE', #147516, .T. ) ;
#134623=VECTOR ( 'NONE', #177476, 1000.000000000000000 ) ;
#134770=DIRECTION ( 'NONE',  ( 1.000000000000000000, -1.145314911736513664E-16, 3.106193895438251016E-17 ) ) ;
#135160=DIRECTION ( 'NONE',  ( 0.000000000000000000, 0.000000000000000000, 1.000000000000000000 ) ) ;
#135235=EDGE_CURVE ( 'NONE', #90818, #39258, #192244, .T. ) ;
#135390=VECTOR ( 'NONE', #250881, 1000.000000000000000 ) ;
#135469=DIRECTION ( 'NONE',  ( -1.000000000000000000, -0.000000000000000000, 0.000000000000000000 ) ) ;
#135545=VECTOR ( 'NONE', #145072, 1000.000000000000000 ) ;
#135659=VERTEX_POINT ( 'NONE', #152831 ) ;
#135787=DIRECTION ( 'NONE',  ( 0.000000000000000000, 0.2617529984164506107, 0.9651348961777299618 ) ) ;
#135985=EDGE_CURVE ( 'NONE', #155667, #36086, #68347, .T. ) ;
#136311=CARTESIAN_POINT ( 'NONE',  ( -16.92973740335368760, 60.88366223094347163, -221.0847067658247056 ) ) ;
#136521=CARTESIAN_POINT ( 'NONE',  ( -16.93262454970420094, 60.86897606381956649, -221.1025001777335888 ) ) ;
#136663=CARTESIAN_POINT ( 'NONE',  ( 20.05000000000002913, 63.54522198573871350, -221.7484608313106378 ) ) ;
#136722=DIRECTION ( 'NONE',  ( 1.000000000000000000, 0.000000000000000000, 0.000000000000000000 ) ) ;
#136892=VERTEX_POINT ( 'NONE', #139851 ) ;
#137049=FACE_OUTER_BOUND ( 'NONE', #211630, .T. ) ;
#137154=LINE ( 'NONE', #156751, #181043 ) ;
#137276=VERTEX_POINT ( 'NONE', #195712 ) ;
#137614=FACE_OUTER_BOUND ( 'NONE', #131519, .T. ) ;
#137676=VERTEX_POINT ( 'NONE', #136663 ) ;
#137692=CARTESIAN_POINT ( 'NONE',  ( -23.25000000000000355, 62.23844973457045882, -209.3750075427748811 ) ) ;
#137713=VECTOR ( 'NONE', #45459, 1000.000000000000000 ) ;
#138027=CARTESIAN_POINT ( 'NONE',  ( -17.71734398241072839, 59.45641310563337356, -223.1004793665990746 ) ) ;
#138189=EDGE_CURVE ( 'NONE', #43158, #133225, #197333, .T. ) ;
#138383=ORIENTED_EDGE ( 'NONE', *, *, #149767, .T. ) ;
#138474=CARTESIAN_POINT ( 'NONE',  ( -16.87333278164134853, 63.02430237963940840, -213.6115832883065195 ) ) ;
#138478=CARTESIAN_POINT ( 'NONE',  ( -18.34804628011471195, 58.57934086597928314, -223.9244941873114101 ) ) ;
#138652=B_SPLINE_CURVE_WITH_KNOTS ( 'NONE', 3,
 ( #58270, #239504, #195262, #81663, #139071, #178268, #255148, #41323, #56977, #120864, #197790, #76563, #136521, #200373, #141669, #21745, #156139, #257712, #235631 ),
 .UNSPECIFIED., .F., .F.,
 ( 4, 3, 3, 3, 3, 3, 4 ),
 ( 0.0001624081864585767763, 0.0001685232196531791216, 0.0001764526673566963095, 0.0001916878551483256420, 0.0002009890782182563310, 0.0002238845907555157540, 0.0002283406619926372746 ),
 .UNSPECIFIED. ) ;
#138777=DIRECTION ( 'NONE',  ( 0.000000000000000000, -0.9651348961777164170, 0.2617529984165006263 ) ) ;
#138924=CIRCLE ( 'NONE', #13893, 0.09999999999999939493 ) ;
#138971=CARTESIAN_POINT ( 'NONE',  ( -16.98495255085919098, 63.03613173686448334, -213.0982309764472689 ) ) ;
#139047=DIRECTION ( 'NONE',  ( -0.000000000000000000, 0.2617529984165031243, 0.9651348961777157509 ) ) ;
#139071=CARTESIAN_POINT ( 'NONE',  ( -16.93909480342659890, 60.88478451565230642, -221.0783736713412679 ) ) ;
#139176=( BOUNDED_CURVE ( )  B_SPLINE_CURVE ( 3, ( #3615, #162718, #57157, #200542 ),
 .UNSPECIFIED., .F., .F. ) 
 B_SPLINE_CURVE_WITH_KNOTS ( ( 4, 4 ),
 ( 1.570796326794935860, 3.141592653589695416 ),
 .UNSPECIFIED. ) 
 CURVE ( )  GEOMETRIC_REPRESENTATION_ITEM ( )  RATIONAL_B_SPLINE_CURVE ( ( 1.000000000000000000, 0.8047378541243972450, 0.8047378541243972450, 1.000000000000000000 ) ) 
 REPRESENTATION_ITEM ( '' )  );
#139195=CARTESIAN_POINT ( 'NONE',  ( -16.97683809663752186, 61.13629130372252973, -220.3155949669961728 ) ) ;
#139703=EDGE_CURVE ( 'NONE', #36086, #88284, #211363, .T. ) ;
#139763=CARTESIAN_POINT ( 'NONE',  ( -16.96982749440682525, 62.96145768098447348, -213.5858467972242636 ) ) ;
#139821=CARTESIAN_POINT ( 'NONE',  ( 12.93225390519046769, 62.16217865953740329, -218.5667261927901279 ) ) ;
#139851=CARTESIAN_POINT ( 'NONE',  ( -18.40000000000000213, 58.56629890316250453, -223.9209570932885356 ) ) ;
#139945=ORIENTED_EDGE ( 'NONE', *, *, #90460, .F. ) ;
#140042=CARTESIAN_POINT ( 'NONE',  ( -17.22767730083624116, 63.03870491652143215, -211.7757501871273860 ) ) ;
#140089=CARTESIAN_POINT ( 'NONE',  ( -17.11825945287481687, 63.05955705323258798, -213.2241350765465597 ) ) ;
#140319=FACE_OUTER_BOUND ( 'NONE', #237799, .T. ) ;
#140593=B_SPLINE_CURVE_WITH_KNOTS ( 'NONE', 3,
 ( #131017, #232709, #189715, #50182, #170203, #132298, #129736, #252240, #250949, #112746 ),
 .UNSPECIFIED., .F., .F.,
 ( 4, 3, 3, 4 ),
 ( 0.000000000000000000, 1.004626015992112955E-05, 1.831183478184268218E-05, 2.062343583996018031E-05 ),
 .UNSPECIFIED. ) ;
#140842=B_SPLINE_CURVE_WITH_KNOTS ( 'NONE', 3,
 ( #162444, #157317, #20369, #179437, #82843, #181994, #56864, #58160, #178160, #743, #217236, #2045, #80280, #239399 ),
 .UNSPECIFIED., .F., .F.,
 ( 4, 2, 2, 2, 2, 2, 4 ),
 ( 0.000000000000000000, 0.0003823333598417312821, 0.0005735000397626380687, 0.0006690833797230922751, 0.0007168750497033180230, 0.0007407708846934308970, 0.0007646667196835437710 ),
 .UNSPECIFIED. ) ;
#141222=TOROIDAL_SURFACE ( 'NONE', #33120, 14.20833333333334103, 0.1000000000000000056 ) ;
#141329=EDGE_CURVE ( 'NONE', #118476, #257876, #210606, .T. ) ;
#141577=CARTESIAN_POINT ( 'NONE',  ( -16.87036670365549895, 60.86740053880574663, -221.1564527318009254 ) ) ;
#141581=ORIENTED_EDGE ( 'NONE', *, *, #93336, .F. ) ;
#141585=ORIENTED_EDGE ( 'NONE', *, *, #77965, .T. ) ;
#141617=DIRECTION ( 'NONE',  ( 1.000000000000000000, 0.000000000000000000, 0.000000000000000000 ) ) ;
#141669=CARTESIAN_POINT ( 'NONE',  ( -16.93583594267724379, 60.85906102366440962, -221.1138329385686063 ) ) ;
#141752=LINE ( 'NONE', #221280, #47634 ) ;
#141774=CARTESIAN_POINT ( 'NONE',  ( -16.89155683852641232, 61.10357422879747702, -220.4362292707147333 ) ) ;
#141847=DIRECTION ( 'NONE',  ( 0.5932847527679309119, 0.7769265190100943519, -0.2107092456252272483 ) ) ;
#142357=CARTESIAN_POINT ( 'NONE',  ( 13.22461703343583572, 62.91973165888628472, -215.7008495347501480 ) ) ;
#142578=CARTESIAN_POINT ( 'NONE',  ( -16.93211319090181632, 63.05646689806795990, -213.0445598095664081 ) ) ;
#142625=CARTESIAN_POINT ( 'NONE',  ( -20.65000000000000568, 63.54522198573874192, -221.7484608313106378 ) ) ;
#142640=DIRECTION ( 'NONE',  ( -0.7071067811865633379, 0.6824534298470439353, -0.1850873201761353837 ) ) ;
#142646=ORIENTED_EDGE ( 'NONE', *, *, #210701, .F. ) ;
#142744=ORIENTED_EDGE ( 'NONE', *, *, #116453, .F. ) ;
#142753=CARTESIAN_POINT ( 'NONE',  ( 18.39999999999999503, 67.23581240663841641, -214.2531594801197627 ) ) ;
#142799=ORIENTED_EDGE ( 'NONE', *, *, #116562, .F. ) ;
#142958=ORIENTED_EDGE ( 'NONE', *, *, #14339, .T. ) ;
#143054=CARTESIAN_POINT ( 'NONE',  ( -16.83558968593871796, 60.94257868581368598, -221.0298515696131005 ) ) ;
#143190=CARTESIAN_POINT ( 'NONE',  ( -16.88219499860498019, 60.93897784699102260, -221.0423399452780870 ) ) ;
#143271=CARTESIAN_POINT ( 'NONE',  ( -18.40000000000000213, 59.20211495293902004, -220.5705723384363921 ) ) ;
#143339=CIRCLE ( 'NONE', #64229, 1.749999999999998002 ) ;
#143530=CARTESIAN_POINT ( 'NONE',  ( 18.39999999999999503, 59.46930106059529209, -220.6430355403071530 ) ) ;
#143678=CARTESIAN_POINT ( 'NONE',  ( 15.74999999999999645, 62.59162599727320497, -217.2417264603073477 ) ) ;
#143688=VECTOR ( 'NONE', #180302, 1000.000000000000000 ) ;
#143765=CIRCLE ( 'NONE', #35671, 14.30833333333335133 ) ;
#143831=AXIS2_PLACEMENT_3D ( 'NONE', #249703, #256056, #115316 ) ;
#143869=CARTESIAN_POINT ( 'NONE',  ( -16.93521499325732549, 63.05745603785386777, -213.0607812399036050 ) ) ;
#144051=CARTESIAN_POINT ( 'NONE',  ( -16.81744102076749314, 60.93935776605891164, -221.0417277355860790 ) ) ;
#144189=( NAMED_UNIT ( * ) SI_UNIT ( $, .STERADIAN. ) SOLID_ANGLE_UNIT ( ) );
#144355=DIRECTION ( 'NONE',  ( -1.000000000000000000, -2.808674667590276147E-16, -1.035613708381807261E-15 ) ) ;
#144494=FACE_OUTER_BOUND ( 'NONE', #256220, .T. ) ;
#144611=FACE_OUTER_BOUND ( 'NONE', #257873, .T. ) ;
#144914=CARTESIAN_POINT ( 'NONE',  ( 14.22916352759892433, 62.94600569631032982, -215.5247064183336363 ) ) ;
#144951=CARTESIAN_POINT ( 'NONE',  ( 15.06592377766033053, 62.16167874586911779, -218.5680441376359227 ) ) ;
#144968=CIRCLE ( 'NONE', #199145, 1.500000000000001332 ) ;
#145008=EDGE_CURVE ( 'NONE', #172263, #75669, #227315, .T. ) ;
#145072=DIRECTION ( 'NONE',  ( -1.000000000000000000, 0.000000000000000000, 0.000000000000000000 ) ) ;
#145233=CARTESIAN_POINT ( 'NONE',  ( -17.11825945287481332, 62.98921886345647181, -213.1014462870871284 ) ) ;
#145328=EDGE_CURVE ( 'NONE', #21828, #211757, #153478, .T. ) ;
#145413=VERTEX_POINT ( 'NONE', #4657 ) ;
#145602=ORIENTED_EDGE ( 'NONE', *, *, #210018, .F. ) ;
#145675=CARTESIAN_POINT ( 'NONE',  ( -15.55912972643741199, 62.34761478309390981, -221.4236593165597071 ) ) ;
#145697=CARTESIAN_POINT ( 'NONE',  ( -15.69373346032659811, 62.70412490954451101, -216.8009802157223476 ) ) ;
#145892=CARTESIAN_POINT ( 'NONE',  ( 18.39999999999999147, 61.13752757784637026, -224.6182967272386009 ) ) ;
#146035=ORIENTED_EDGE ( 'NONE', *, *, #108970, .T. ) ;
#146129=VERTEX_POINT ( 'NONE', #18511 ) ;
#146204=CARTESIAN_POINT ( 'NONE',  ( 15.73863059295127087, 62.65035202501399425, -217.0198313409406978 ) ) ;
#146616=CARTESIAN_POINT ( 'NONE',  ( -16.89020380669787613, 60.96747295614021311, -220.9380614883060900 ) ) ;
#146683=CARTESIAN_POINT ( 'NONE',  ( -18.44085059012131822, 58.54245214771228234, -223.9044447480369513 ) ) ;
#146975=CARTESIAN_POINT ( 'NONE',  ( -12.33960340485503693, 62.72902952540357546, -216.6940264888115166 ) ) ;
#147026=ORIENTED_EDGE ( 'NONE', *, *, #125672, .F. ) ;
#147143=FILL_AREA_STYLE ('',( #105416 ) ) ;
#147218=DIRECTION ( 'NONE',  ( 0.000000000000000000, -0.8446299136406466568, 0.5353506411534347809 ) ) ;
#147232=ORIENTED_EDGE ( 'NONE', *, *, #158908, .F. ) ;
#147263=DIRECTION ( 'NONE',  ( 1.000000000000000000, 0.000000000000000000, 0.000000000000000000 ) ) ;
#147516=EDGE_LOOP ( 'NONE', ( #145602, #93524, #154788, #172100 ) ) ;
#147660=LINE ( 'NONE', #87666, #215556 ) ;
#147734=ORIENTED_EDGE ( 'NONE', *, *, #217472, .T. ) ;
#147761=CARTESIAN_POINT ( 'NONE',  ( -18.39999999999999858, 58.59921997668411819, -223.8511959880075608 ) ) ;
#147933=CARTESIAN_POINT ( 'NONE',  ( -16.97048326478265778, 61.06790646447517901, -220.5677433478223861 ) ) ;
#148088=PLANE ( 'NONE',  #75648 ) ;
#148094=CARTESIAN_POINT ( 'NONE',  ( -16.81453046979151367, 60.96603263716392007, -220.9850058241458726 ) ) ;
#148157=EDGE_CURVE ( 'NONE', #243144, #50473, #221031, .T. ) ;
#148166=CARTESIAN_POINT ( 'NONE',  ( -16.77683809663752257, 63.08573235307424198, -213.1276215869287967 ) ) ;
#148210=EDGE_CURVE ( 'NONE', #124122, #115941, #123436, .T. ) ;
#148282=CARTESIAN_POINT ( 'NONE',  ( -13.77083647240106146, 62.94600569631032982, -215.5247064183336363 ) ) ;
#148352=LINE ( 'NONE', #173100, #186333 ) ;
#148382=EDGE_CURVE ( 'NONE', #240443, #205367, #211762, .T. ) ;
#148460=DIRECTION ( 'NONE',  ( 0.000000000000000000, 0.2617529984165031243, 0.9651348961777157509 ) ) ;
#148683=ADVANCED_FACE ( 'NONE', ( #137049 ), #106558, .F. ) ;
#148797=CARTESIAN_POINT ( 'NONE',  ( 12.25000000000000000, 62.59162599727320497, -217.2417264603073761 ) ) ;
#148949=CARTESIAN_POINT ( 'NONE',  ( -16.97683809663752186, 62.98531230502843670, -213.8799296553602005 ) ) ;
#148983=CARTESIAN_POINT ( 'NONE',  ( 21.72449340488910607, 59.72708471423849375, -224.2357723256170061 ) ) ;
#149248=ADVANCED_FACE ( 'NONE', ( #209223 ), #206664, .F. ) ;
#149249=CARTESIAN_POINT ( 'NONE',  ( 18.39999999999999503, 65.08943781962308606, -222.1672656287770451 ) ) ;
#149767=EDGE_CURVE ( 'NONE', #180612, #75872, #127894, .T. ) ;
#149837=ORIENTED_EDGE ( 'NONE', *, *, #252944, .F. ) ;
#151040=DIRECTION ( 'NONE',  ( -1.073024830501117725E-15, -0.2617529984165031243, -0.9651348961777157509 ) ) ;
#151077=VERTEX_POINT ( 'NONE', #164505 ) ;
#151242=CIRCLE ( 'NONE', #234610, 14.20833333333334103 ) ;
#151244=LINE ( 'NONE', #73009, #112081 ) ;
#151275=CARTESIAN_POINT ( 'NONE',  ( -16.77683809663752257, 60.94702803318471496, -221.0293550571836647 ) ) ;
#151375=CARTESIAN_POINT ( 'NONE',  ( 12.25000000000000000, 62.62153588618860311, -217.1314428046943590 ) ) ;
#151461=CARTESIAN_POINT ( 'NONE',  ( -16.94107738177415712, 60.85118289042637940, -221.1214263997032106 ) ) ;
#151566=CIRCLE ( 'NONE', #68343, 1.749999999999999778 ) ;
#151647=DIRECTION ( 'NONE',  ( 0.000000000000000000, -0.9651348961777157509, 0.2617529984165031243 ) ) ;
#151882=CARTESIAN_POINT ( 'NONE',  ( -18.37013991200266005, 58.54242066476462014, -223.9590583060466997 ) ) ;
#151967=CARTESIAN_POINT ( 'NONE',  ( -16.85312841634288006, 61.03918102309979332, -220.8126985114581942 ) ) ;
#152048=DIRECTION ( 'NONE',  ( 1.000000000000000000, 0.000000000000000000, -0.000000000000000000 ) ) ;
#152057=EDGE_CURVE ( 'NONE', #58353, #75872, #223016, .T. ) ;
#152100=EDGE_LOOP ( 'NONE', ( #87366, #116755, #166726, #92100, #238354, #36829, #171579, #39699, #156738, #176793, #176448, #30322, #22231, #109845 ) ) ;
#152269=ORIENTED_EDGE ( 'NONE', *, *, #47376, .F. ) ;
#152547=DIRECTION ( 'NONE',  ( -1.000000000000000000, 1.560919790631901733E-14, -5.345137975828415463E-15 ) ) ;
#152711=CYLINDRICAL_SURFACE ( 'NONE', #15985, 1.749999999999998002 ) ;
#152831=CARTESIAN_POINT ( 'NONE',  ( -16.77683809663752257, 63.08610022504904435, -213.1421742787362064 ) ) ;
#152959=ORIENTED_EDGE ( 'NONE', *, *, #232770, .T. ) ;
#152990=CARTESIAN_POINT ( 'NONE',  ( -15.70407651835961360, 62.46590406472956403, -217.6831045281099932 ) ) ;
#153083=FACE_OUTER_BOUND ( 'NONE', #23840, .T. ) ;
#153124=DIRECTION ( 'NONE',  ( 1.186688945009009831E-16, 0.9651348961777157509, -0.2617529984165031243 ) ) ;
#153197=CARTESIAN_POINT ( 'NONE',  ( 20.73486653747090003, 65.69159657275403674, -213.8343546826533554 ) ) ;
#153259=CARTESIAN_POINT ( 'NONE',  ( -16.87683809663752399, 61.23280479334025017, -220.3417702668379832 ) ) ;
#153272=DIRECTION ( 'NONE',  ( 1.000000000000000000, -2.808674667590276147E-16, -1.035613708381807261E-15 ) ) ;
#153478=CIRCLE ( 'NONE', #3573, 0.1999999999999987899 ) ;
#153513=CARTESIAN_POINT ( 'NONE',  ( 0.000000000000000000, 0.000000000000000000, 0.000000000000000000 ) ) ;
#153527=CARTESIAN_POINT ( 'NONE',  ( -16.89268316805466341, 60.93619025550653134, -221.0468289635910537 ) ) ;
#153541=CARTESIAN_POINT ( 'NONE',  ( 23.24999999999999645, 65.08943781962308606, -222.1672656287770451 ) ) ;
#153773=LINE ( 'NONE', #169475, #92566 ) ;
#153853=EDGE_CURVE ( 'NONE', #118873, #6716, #38145, .T. ) ;
#154021=PLANE ( 'NONE',  #88433 ) ;
#154788=ORIENTED_EDGE ( 'NONE', *, *, #20234, .F. ) ;
#154871=ADVANCED_FACE ( 'NONE', ( #179222 ), #78312, .T. ) ;
#155002=CARTESIAN_POINT ( 'NONE',  ( -17.05016517655894148, 60.94529903456965059, -221.0198211075746713 ) ) ;
#155040=B_SPLINE_CURVE_WITH_KNOTS ( 'NONE', 3,
 ( #30857, #12572, #131201, #189903 ),
 .UNSPECIFIED., .F., .F.,
 ( 4, 4 ),
 ( 0.000000000000000000, 7.713889350930169559E-05 ),
 .UNSPECIFIED. ) ;
#155159=DIRECTION ( 'NONE',  ( 1.000000000000000000, 0.000000000000000000, 0.000000000000000000 ) ) ;
#155309=CARTESIAN_POINT ( 'NONE',  ( -16.87304349924914604, 63.08462258781068499, -213.0868426661930641 ) ) ;
#155345=VERTEX_POINT ( 'NONE', #87477 ) ;
#155537=CARTESIAN_POINT ( 'NONE',  ( -16.87401514999228880, 63.06741435278433272, -213.1951636644405710 ) ) ;
#155589=CARTESIAN_POINT ( 'NONE',  ( -16.87331047859651179, 60.93935776605891164, -221.0417277355860790 ) ) ;
#155659=ORIENTED_EDGE ( 'NONE', *, *, #179608, .T. ) ;
#155667=VERTEX_POINT ( 'NONE', #218986 ) ;
#155823=FACE_OUTER_BOUND ( 'NONE', #49308, .T. ) ;
#155915=AXIS2_PLACEMENT_3D ( 'NONE', #252585, #231765, #229196 ) ;
#155937=CARTESIAN_POINT ( 'NONE',  ( -16.89318236219976299, 60.93653333852449805, -221.0462766641838357 ) ) ;
#156030=CARTESIAN_POINT ( 'NONE',  ( -17.04761207306819770, 63.01194694731475465, -213.1076103415853993 ) ) ;
#156139=CARTESIAN_POINT ( 'NONE',  ( -16.93970660449832621, 60.85312929741117927, -221.1195901196794580 ) ) ;
#156144=DIRECTION ( 'NONE',  ( 1.073024830501117725E-15, 0.2617529984165031243, 0.9651348961777157509 ) ) ;
#156334=PLANE ( 'NONE',  #3020 ) ;
#156431=CARTESIAN_POINT ( 'NONE',  ( -16.78055652883087134, 60.94529327262787177, -221.0321558084000912 ) ) ;
#156600=CARTESIAN_POINT ( 'NONE',  ( -16.86578989773640558, 63.08215007703680755, -213.0078429336296608 ) ) ;
#156721=CARTESIAN_POINT ( 'NONE',  ( -16.97683809663752186, 62.88879881541066652, -213.8537543555185607 ) ) ;
#156738=ORIENTED_EDGE ( 'NONE', *, *, #224783, .F. ) ;
#156751=CARTESIAN_POINT ( 'NONE',  ( 21.13736287352038445, 61.88639443390047745, -224.8213959476306911 ) ) ;
#156824=CARTESIAN_POINT ( 'NONE',  ( -18.40000000000000213, 58.56629890316250453, -223.9209570932885356 ) ) ;
#156899=DIRECTION ( 'NONE',  ( -1.000000000000000000, -1.594516344651357984E-15, 4.324467345337419894E-16 ) ) ;
#157075=EDGE_CURVE ( 'NONE', #237838, #38064, #88185, .T. ) ;
#157088=B_SPLINE_CURVE_WITH_KNOTS ( 'NONE', 3,
 ( #35203, #216358, #212536, #37753, #117273, #211232, #156431, #73045, #170880, #175982, #91293, #250361, #151275 ),
 .UNSPECIFIED., .F., .F.,
 ( 4, 3, 3, 3, 4 ),
 ( 1.077764583621373145E-16, 1.946463881814408957E-05, 3.922356109942842209E-05, 4.215060953236330466E-05, 4.415117091090545512E-05 ),
 .UNSPECIFIED. ) ;
#157312=EDGE_CURVE ( 'NONE', #172263, #10339, #67352, .T. ) ;
#157317=CARTESIAN_POINT ( 'NONE',  ( -16.87683809663752754, 63.00406867418889334, -213.7537959572469788 ) ) ;
#158243=EDGE_LOOP ( 'NONE', ( #214624, #155659, #74635, #98771 ) ) ;
#158255=ORIENTED_EDGE ( 'NONE', *, *, #105533, .T. ) ;
#158384=CARTESIAN_POINT ( 'NONE',  ( -16.91256925476569606, 63.08204023972218977, -213.0047279777397193 ) ) ;
#158390=CARTESIAN_POINT ( 'NONE',  ( -16.94389599337535657, 63.05705733563543447, -213.0759594097623335 ) ) ;
#158415=ORIENTED_EDGE ( 'NONE', *, *, #54667, .T. ) ;
#158418=CARTESIAN_POINT ( 'NONE',  ( -18.40000000000000213, 62.23844973457045882, -209.3750075427748811 ) ) ;
#158420=CARTESIAN_POINT ( 'NONE',  ( -16.87683809663752399, 48.78215419113038109, -213.4964773079645681 ) ) ;
#158519=AXIS2_PLACEMENT_3D ( 'NONE', #214132, #38079, #173775 ) ;
#158643=VERTEX_POINT ( 'NONE', #225246 ) ;
#158683=CARTESIAN_POINT ( 'NONE',  ( -23.25000000000000355, 67.23581240663841641, -214.2531594801197627 ) ) ;
#158734=FACE_OUTER_BOUND ( 'NONE', #73037, .T. ) ;
#158908=EDGE_CURVE ( 'NONE', #172111, #158643, #188013, .T. ) ;
#158976=FACE_OUTER_BOUND ( 'NONE', #23338, .T. ) ;
#159079=DIRECTION ( 'NONE',  ( -0.000000000000000000, 0.2617529984165031243, 0.9651348961777157509 ) ) ;
#159388=DIRECTION ( 'NONE',  ( 1.000000000000000000, 0.000000000000000000, 0.000000000000000000 ) ) ;
#159637=CARTESIAN_POINT ( 'NONE',  ( -17.29838795458127976, 63.00731216765596798, -211.8062850501013088 ) ) ;
#159771=CARTESIAN_POINT ( 'NONE',  ( -16.90202395485713183, 60.91009262921385670, -221.0887195956053404 ) ) ;
#159796=EDGE_CURVE ( 'NONE', #116061, #127095, #148352, .T. ) ;
#160075=ADVANCED_FACE ( 'NONE', ( #140319 ), #122064, .F. ) ;
#160093=CARTESIAN_POINT ( 'NONE',  ( -16.80070461187903774, 60.93856303923769957, -221.0446580500125435 ) ) ;
#160326=CARTESIAN_POINT ( 'NONE',  ( -21.65000000000000213, 62.65526179112262639, -225.0299194783148948 ) ) ;
#160438=EDGE_CURVE ( 'NONE', #155345, #172111, #28943, .T. ) ;
#160647=EDGE_CURVE ( 'NONE', #32098, #67123, #192023, .T. ) ;
#160972=LINE ( 'NONE', #237918, #94276 ) ;
#160976=CARTESIAN_POINT ( 'NONE',  ( -17.11825945287481332, 63.08573235307419935, -213.1276215869287967 ) ) ;
#161056=CARTESIAN_POINT ( 'NONE',  ( -16.92778301347280490, 60.86963669884748640, -221.1041733168329131 ) ) ;
#161113=CYLINDRICAL_SURFACE ( 'NONE', #27842, 1.749999999999999778 ) ;
#161156=CARTESIAN_POINT ( 'NONE',  ( -16.86757978335471719, 60.91064310117739211, -221.0878137256144100 ) ) ;
#161264=VECTOR ( 'NONE', #173749, 1000.000000000000000 ) ;
#161274=EDGE_CURVE ( 'NONE', #230526, #70322, #19167, .T. ) ;
#161424=AXIS2_PLACEMENT_3D ( 'NONE', #41786, #238675, #22215 ) ;
#161480=ORIENTED_EDGE ( 'NONE', *, *, #28230, .T. ) ;
#161884=DIRECTION ( 'NONE',  ( 1.000000000000000000, 0.000000000000000000, -0.000000000000000000 ) ) ;
#162012=DIRECTION ( 'NONE',  ( 1.000000000000000000, 0.000000000000000000, 0.000000000000000000 ) ) ;
#162444=CARTESIAN_POINT ( 'NONE',  ( -16.87683809663752399, 62.98531230502843670, -213.8799296553602005 ) ) ;
#162449=CARTESIAN_POINT ( 'NONE',  ( -16.86578989773641979, 60.87574773424856289, -221.1432832491776992 ) ) ;
#162647=CARTESIAN_POINT ( 'NONE',  ( -16.87333278164111050, 61.13086903662161831, -220.5930452161097719 ) ) ;
#162688=VECTOR ( 'NONE', #2167, 1000.000000000000000 ) ;
#162718=CARTESIAN_POINT ( 'NONE',  ( -18.40000000000000213, 59.52583735386146202, -220.6583686759552734 ) ) ;
#162822=CARTESIAN_POINT ( 'NONE',  ( -16.78805706634180339, 63.08588851766376848, -213.1337219450663270 ) ) ;
#162852=EDGE_CURVE ( 'NONE', #96731, #5980, #103977, .T. ) ;
#162933=CARTESIAN_POINT ( 'NONE',  ( 20.99999999999999645, 60.24242455067834356, -224.3755369822736156 ) ) ;
#162989=ORIENTED_EDGE ( 'NONE', *, *, #20234, .T. ) ;
#163006=ORIENTED_EDGE ( 'NONE', *, *, #256578, .T. ) ;
#163205=VECTOR ( 'NONE', #64732, 1000.000000000000000 ) ;
#163262=CARTESIAN_POINT ( 'NONE',  ( 18.39999999999998082, 58.57934086597919077, -223.9244941873113817 ) ) ;
#163271=VERTEX_POINT ( 'NONE', #89485 ) ;
#163451=CARTESIAN_POINT ( 'NONE',  ( -16.94107738177414291, 63.04990807712500356, -213.0142932718104021 ) ) ;
#163536=CIRCLE ( 'NONE', #196841, 0.09999999999999543976 ) ;
#163999=EDGE_LOOP ( 'NONE', ( #187174, #238644, #27596, #252400, #54642, #63648, #195222, #142744, #8869, #164967, #251194, #168602 ) ) ;
#164002=CARTESIAN_POINT ( 'NONE',  ( -15.73854595235691534, 62.65055472571233253, -217.0190438104121995 ) ) ;
#164067=CARTESIAN_POINT ( 'NONE',  ( 23.04999999999999716, 62.02748777246247869, -221.3368380802343722 ) ) ;
#164235=VECTOR ( 'NONE', #83992, 1000.000000000000000 ) ;
#164407=ORIENTED_EDGE ( 'NONE', *, *, #162852, .F. ) ;
#164505=CARTESIAN_POINT ( 'NONE',  ( -12.25000000000000178, 62.59162599727320497, -217.2417264603073477 ) ) ;
#164512=CARTESIAN_POINT ( 'NONE',  ( 15.07585980824112681, 62.89253001998300618, -215.8738493471900597 ) ) ;
#164530=CARTESIAN_POINT ( 'NONE',  ( 23.24999999999999645, 59.20211495293902715, -220.5705723384363637 ) ) ;
#164547=CARTESIAN_POINT ( 'NONE',  ( 15.39793903038207823, 62.27137470634864513, -218.2709398499965801 ) ) ;
#164720=( GEOMETRIC_REPRESENTATION_CONTEXT ( 3 ) GLOBAL_UNCERTAINTY_ASSIGNED_CONTEXT ( ( #52937 ) ) GLOBAL_UNIT_ASSIGNED_CONTEXT ( ( #226677, #166754, #247539 ) ) REPRESENTATION_CONTEXT ( 'NONE', 'WORKASPACE' ) );
#164967=ORIENTED_EDGE ( 'NONE', *, *, #63063, .F. ) ;
#165128=DIRECTION ( 'NONE',  ( -1.020425574104004196E-15, -0.2617529984165031243, -0.9651348961777157509 ) ) ;
#165272=AXIS2_PLACEMENT_3D ( 'NONE', #250103, #27237, #8925 ) ;
#165313=CARTESIAN_POINT ( 'NONE',  ( 21.72449340488910252, 60.61704490885460217, -220.9543136786127491 ) ) ;
#165437=FACE_BOUND ( 'NONE', #79712, .T. ) ;
#165488=ORIENTED_EDGE ( 'NONE', *, *, #178243, .T. ) ;
#165672=CARTESIAN_POINT ( 'NONE',  ( -12.93407622233967658, 62.16167874586912490, -218.5680441376359795 ) ) ;
#165891=CARTESIAN_POINT ( 'NONE',  ( -16.94445028196808778, 60.88759175473954599, -221.0718995934454938 ) ) ;
#166136=CARTESIAN_POINT ( 'NONE',  ( -16.93388492042257809, 63.06176463275114941, -213.0687502871022616 ) ) ;
#166275=VERTEX_POINT ( 'NONE', #14616 ) ;
#166585=CARTESIAN_POINT ( 'NONE',  ( 20.09999999999999787, 61.13238474529445909, -221.0940783352693586 ) ) ;
#166726=ORIENTED_EDGE ( 'NONE', *, *, #179441, .F. ) ;
#166744=CYLINDRICAL_SURFACE ( 'NONE', #183532, 14.30833333333335133 ) ;
#166754=( NAMED_UNIT ( * ) PLANE_ANGLE_UNIT ( ) SI_UNIT ( $, .RADIAN. ) );
#167189=CARTESIAN_POINT ( 'NONE',  ( -17.11825945287482753, 60.84284427644114146, -221.0155524357444108 ) ) ;
#167219=ORIENTED_EDGE ( 'NONE', *, *, #182391, .T. ) ;
#167346=EDGE_CURVE ( 'NONE', #77430, #180046, #99897, .T. ) ;
#167660=LINE ( 'NONE', #189767, #16584 ) ;
#167764=PLANE ( 'NONE',  #71092 ) ;
#167970=CARTESIAN_POINT ( 'NONE',  ( -16.80939487329395021, 63.08573235307446225, -213.1276215869279724 ) ) ;
#168043=DIRECTION ( 'NONE',  ( 1.186688945009010077E-16, 0.9651348961777157509, -0.2617529984165031243 ) ) ;
#168071=VERTEX_POINT ( 'NONE', #81970 ) ;
#168212=CARTESIAN_POINT ( 'NONE',  ( 20.27550659511089037, 61.64772458173430181, -221.2338429919259966 ) ) ;
#168224=CIRCLE ( 'NONE', #230554, 1.749999999999998002 ) ;
#168448=CARTESIAN_POINT ( 'NONE',  ( -21.65000000000000213, 62.65526179112262639, -225.0299194783148948 ) ) ;
#168602=ORIENTED_EDGE ( 'NONE', *, *, #59660, .F. ) ;
#168647=LINE ( 'NONE', #108616, #229778 ) ;
#168982=CARTESIAN_POINT ( 'NONE',  ( -16.83199030136658081, 60.99007385930059399, -220.9286596726492746 ) ) ;
#169104=VECTOR ( 'NONE', #241187, 1000.000000000000000 ) ;
#169162=CARTESIAN_POINT ( 'NONE',  ( -15.51798037960204013, 62.79576509294744824, -216.3871738676108976 ) ) ;
#169218=FACE_OUTER_BOUND ( 'NONE', #255110, .T. ) ;
#169240=DIRECTION ( 'NONE',  ( 0.000000000000000000, -0.9651348961777157509, 0.2617529984165031243 ) ) ;
#169444=DIRECTION ( 'NONE',  ( 1.000000000000000000, -4.625929269271478222E-14, 0.000000000000000000 ) ) ;
#169475=CARTESIAN_POINT ( 'NONE',  ( 20.27550659511089037, 63.79409916874963216, -213.3197368432687426 ) ) ;
#169653=SHAPE_DEFINITION_REPRESENTATION ( #224130, #198303 ) ;
#169680=CARTESIAN_POINT ( 'NONE',  ( 12.33938619321247820, 62.72888572355475389, -216.6946536606585880 ) ) ;
#169792=( BOUNDED_CURVE ( )  B_SPLINE_CURVE ( 3, ( #180938, #119690, #239632, #182225 ),
 .UNSPECIFIED., .F., .F. ) 
 B_SPLINE_CURVE_WITH_KNOTS ( ( 4, 4 ),
 ( 2.589852378279007272, 2.850972632318391042 ),
 .UNSPECIFIED. ) 
 CURVE ( )  GEOMETRIC_REPRESENTATION_ITEM ( )  RATIONAL_B_SPLINE_CURVE ( ( 1.000000000000000000, 0.9943260843901262636, 0.9943260843901262636, 1.000000000000000000 ) ) 
 REPRESENTATION_ITEM ( '' )  );
#169805=ORIENTED_EDGE ( 'NONE', *, *, #5494, .T. ) ;
#169915=ORIENTED_EDGE ( 'NONE', *, *, #194505, .F. ) ;
#169979=AXIS2_PLACEMENT_3D ( 'NONE', #202871, #24263, #25538 ) ;
#170180=FACE_OUTER_BOUND ( 'NONE', #68919, .T. ) ;
#170186=EDGE_CURVE ( 'NONE', #155345, #137276, #29066, .T. ) ;
#170203=CARTESIAN_POINT ( 'NONE',  ( -16.88593481969334320, 63.08568185945787121, -213.1256680011580897 ) ) ;
#170402=CARTESIAN_POINT ( 'NONE',  ( 15.48841904831874849, 62.27936944010919973, -221.4051505845420991 ) ) ;
#170746=CARTESIAN_POINT ( 'NONE',  ( -16.95709691156655907, 60.94199036320039653, -221.0320208310369026 ) ) ;
#170755=AXIS2_PLACEMENT_3D ( 'NONE', #123516, #203039, #27011 ) ;
#170880=CARTESIAN_POINT ( 'NONE',  ( -16.77902162784672768, 60.94595240997173136, -221.0310918376485745 ) ) ;
#171046=EDGE_CURVE ( 'NONE', #230526, #135659, #131371, .T. ) ;
#171104=CARTESIAN_POINT ( 'NONE',  ( 18.39999999999997371, 62.50563584222673796, -209.4474707446456421 ) ) ;
#171454=CARTESIAN_POINT ( 'NONE',  ( -18.41431012584568094, 58.55944756805622120, -223.9431743560560335 ) ) ;
#171483=VECTOR ( 'NONE', #56841, 1000.000000000000000 ) ;
#171536=CARTESIAN_POINT ( 'NONE',  ( -16.81930730667007623, 60.97200056715625749, -220.9710398144006547 ) ) ;
#171579=ORIENTED_EDGE ( 'NONE', *, *, #148210, .F. ) ;
#171741=CARTESIAN_POINT ( 'NONE',  ( -18.40000000000000213, 62.23844973457045882, -209.3750075427748527 ) ) ;
#172100=ORIENTED_EDGE ( 'NONE', *, *, #224797, .F. ) ;
#172102=VECTOR ( 'NONE', #68841, 1000.000000000000000 ) ;
#172111=VERTEX_POINT ( 'NONE', #5015 ) ;
#172263=VERTEX_POINT ( 'NONE', #8899 ) ;
#172502=ORIENTED_EDGE ( 'NONE', *, *, #158908, .T. ) ;
#172692=PLANE ( 'NONE',  #118172 ) ;
#173100=CARTESIAN_POINT ( 'NONE',  ( -18.40000000000000213, 67.23581240663841641, -214.2531594801197627 ) ) ;
#173115=EDGE_CURVE ( 'NONE', #135659, #172263, #35496, .T. ) ;
#173473=FACE_OUTER_BOUND ( 'NONE', #216622, .T. ) ;
#173677=ORIENTED_EDGE ( 'NONE', *, *, #14568, .F. ) ;
#173749=DIRECTION ( 'NONE',  ( -0.000000000000000000, 0.2617529984165031243, 0.9651348961777157509 ) ) ;
#173775=DIRECTION ( 'NONE',  ( 1.000000000000000000, 0.000000000000000000, 0.000000000000000000 ) ) ;
#173964=CARTESIAN_POINT ( 'NONE',  ( -18.40000000000000213, 65.06382255409391746, -210.1412732845728897 ) ) ;
#173982=ORIENTED_EDGE ( 'NONE', *, *, #103304, .T. ) ;
#174371=CARTESIAN_POINT ( 'NONE',  ( -18.40000000000000213, 62.49385230547966330, -209.4698601954371213 ) ) ;
#174395=CARTESIAN_POINT ( 'NONE',  ( -18.38817693311004575, 62.49759664249535263, -209.4452904435883625 ) ) ;
#174424=ORIENTED_EDGE ( 'NONE', *, *, #118413, .T. ) ;
#174616=EDGE_CURVE ( 'NONE', #136892, #145413, #71157, .T. ) ;
#174664=VERTEX_POINT ( 'NONE', #52841 ) ;
#175115=CARTESIAN_POINT ( 'NONE',  ( -16.87683809663752044, 62.88879881541065942, -213.8537543555185607 ) ) ;
#175133=ADVANCED_FACE ( 'NONE', ( #57662 ), #128579, .F. ) ;
#175134=CARTESIAN_POINT ( 'NONE',  ( -15.06774609480954474, 62.16217865953741750, -218.5667261927900995 ) ) ;
#175364=CARTESIAN_POINT ( 'NONE',  ( -21.65000000000000213, 60.96553306590055854, -220.9452142459683159 ) ) ;
#175494=FACE_OUTER_BOUND ( 'NONE', #19313, .T. ) ;
#175620=CARTESIAN_POINT ( 'NONE',  ( -16.94333152886236249, 60.88942040374450215, -221.0717341904871489 ) ) ;
#175660=DIRECTION ( 'NONE',  ( 0.000000000000000000, -0.2617529984165031243, -0.9651348961777157509 ) ) ;
#175982=CARTESIAN_POINT ( 'NONE',  ( -16.77828822508139694, 60.94630241056517406, -221.0305267419277868 ) ) ;
#176141=EDGE_LOOP ( 'NONE', ( #98710, #234978, #199550, #21388 ) ) ;
#176373=CARTESIAN_POINT ( 'NONE',  ( -16.88783316861815109, 63.05896443345586277, -213.2263201824675889 ) ) ;
#176432=ORIENTED_EDGE ( 'NONE', *, *, #249196, .T. ) ;
#176448=ORIENTED_EDGE ( 'NONE', *, *, #218391, .T. ) ;
#176465=PLANE ( 'NONE',  #220663 ) ;
#176793=ORIENTED_EDGE ( 'NONE', *, *, #179608, .F. ) ;
#176978=EDGE_LOOP ( 'NONE', ( #208899, #55569 ) ) ;
#177297=CARTESIAN_POINT ( 'NONE',  ( -16.97683809663752186, 61.03587125567668181, -221.0679030354277188 ) ) ;
#177437=( BOUNDED_CURVE ( )  B_SPLINE_CURVE ( 3, ( #151461, #251819, #250534, #190589 ),
 .UNSPECIFIED., .F., .T. ) 
 B_SPLINE_CURVE_WITH_KNOTS ( ( 4, 4 ),
 ( 0.3000847527772366186, 0.5497968875596810356 ),
 .UNSPECIFIED. ) 
 CURVE ( )  GEOMETRIC_REPRESENTATION_ITEM ( )  RATIONAL_B_SPLINE_CURVE ( ( 1.000000000000000000, 0.9948104011409419911, 0.9948104011409419911, 1.000000000000000000 ) ) 
 REPRESENTATION_ITEM ( '' )  );
#177476=DIRECTION ( 'NONE',  ( -1.000000000000000000, -0.000000000000000000, 0.000000000000000000 ) ) ;
#177603=CYLINDRICAL_SURFACE ( 'NONE', #158519, 1.749999999999998002 ) ;
#177755=DIRECTION ( 'NONE',  ( 0.000000000000000000, -0.2617529984165031243, -0.9651348961777157509 ) ) ;
#177931=CARTESIAN_POINT ( 'NONE',  ( -16.93301857435210422, 63.06970463974469254, -213.0862067822817778 ) ) ;
#178160=CARTESIAN_POINT ( 'NONE',  ( -16.81453563122428463, 63.08009114446584675, -213.1900633619857501 ) ) ;
#178243=EDGE_CURVE ( 'NONE', #155345, #237838, #32030, .T. ) ;
#178268=CARTESIAN_POINT ( 'NONE',  ( -16.93772744219066340, 60.88373978801495667, -221.0804579231064793 ) ) ;
#178376=CARTESIAN_POINT ( 'NONE',  ( -16.77431908686105544, 60.94711240597669644, -221.0291585267142125 ) ) ;
#178574=ORIENTED_EDGE ( 'NONE', *, *, #46303, .T. ) ;
#178648=LINE ( 'NONE', #258099, #40425 ) ;
#178955=CARTESIAN_POINT ( 'NONE',  ( -16.87683809663752399, 63.00529667655239763, -213.7455378284023482 ) ) ;
#179188=CARTESIAN_POINT ( 'NONE',  ( -16.93589915522258948, 63.05285544833442657, -213.0248735350789389 ) ) ;
#179217=EDGE_CURVE ( 'NONE', #88284, #51883, #99374, .T. ) ;
#179222=FACE_OUTER_BOUND ( 'NONE', #70385, .T. ) ;
#179346=DIRECTION ( 'NONE',  ( -1.186688945009010077E-16, -0.9651348961777154178, 0.2617529984165037904 ) ) ;
#179437=CARTESIAN_POINT ( 'NONE',  ( -16.85939681242906119, 63.04778223063582487, -213.4386086703495948 ) ) ;
#179441=EDGE_CURVE ( 'NONE', #137676, #77226, #144968, .T. ) ;
#179608=EDGE_CURVE ( 'NONE', #7786, #166275, #203438, .T. ) ;
#179633=VERTEX_POINT ( 'NONE', #47947 ) ;
#179651=CARTESIAN_POINT ( 'NONE',  ( -16.87401514999236696, 60.95767576634881380, -220.9741856580743331 ) ) ;
#179875=PLANE ( 'NONE',  #100443 ) ;
#179989=DIRECTION ( 'NONE',  ( 0.000000000000000000, 0.9651348961777157509, -0.2617529984165031243 ) ) ;
#180046=VERTEX_POINT ( 'NONE', #60457 ) ;
#180089=ORIENTED_EDGE ( 'NONE', *, *, #237248, .T. ) ;
#180297=DIRECTION ( 'NONE',  ( -0.7071067811865487940, -0.6824534298470361637, 0.1850873201762206766 ) ) ;
#180302=DIRECTION ( 'NONE',  ( 0.000000000000000000, -0.2617529984165031243, -0.9651348961777157509 ) ) ;
#180612=VERTEX_POINT ( 'NONE', #200974 ) ;
#180778=FILL_AREA_STYLE_COLOUR ( '', #131420 ) ;
#180784=EDGE_LOOP ( 'NONE', ( #219175, #131946, #86718, #199274, #110713 ) ) ;
#180864=VECTOR ( 'NONE', #169240, 1000.000000000000000 ) ;
#180938=CARTESIAN_POINT ( 'NONE',  ( 18.39999999999998082, 58.57934086597919077, -223.9244941873113817 ) ) ;
#181043=VECTOR ( 'NONE', #210592, 1000.000000000000000 ) ;
#181184=ORIENTED_EDGE ( 'NONE', *, *, #37348, .F. ) ;
#181297=DIRECTION ( 'NONE',  ( -0.000000000000000000, 0.2617529984165031243, 0.9651348961777157509 ) ) ;
#181551=CARTESIAN_POINT ( 'NONE',  ( 13.88302573338720869, 62.02991417940920371, -218.9025163457276904 ) ) ;
#181554=CARTESIAN_POINT ( 'NONE',  ( 20.73486653747088582, 62.65526179112259086, -225.0299194783148664 ) ) ;
#181635=ORIENTED_EDGE ( 'NONE', *, *, #198656, .T. ) ;
#181651=DIRECTION ( 'NONE',  ( -1.000000000000000000, 0.000000000000000000, 0.000000000000000000 ) ) ;
#181768=CARTESIAN_POINT ( 'NONE',  ( -18.37013991200266005, 62.49123844501968961, -209.3989888458036148 ) ) ;
#181804=DIRECTION ( 'NONE',  ( -1.000000000000000000, -0.000000000000000000, 0.000000000000000000 ) ) ;
#181838=CARTESIAN_POINT ( 'NONE',  ( -16.89268316805465986, 63.08557629953710943, -213.1216189793661329 ) ) ;
#181906=CARTESIAN_POINT ( 'NONE',  ( -18.40000000000000213, 61.67221194087674263, -212.7442625272979058 ) ) ;
#181919=CARTESIAN_POINT ( 'NONE',  ( -16.97683809663753252, 61.10204373784839049, -220.4418724925039044 ) ) ;
#181955=ADVANCED_FACE ( 'NONE', ( #65044 ), #179875, .F. ) ;
#181994=CARTESIAN_POINT ( 'NONE',  ( -16.83794479845802172, 63.06835707360122711, -213.2820116777518535 ) ) ;
#182058=CARTESIAN_POINT ( 'NONE',  ( 16.87683809663749557, 63.08573235307424198, -213.1276215869287967 ) ) ;
#182148=EDGE_CURVE ( 'NONE', #66925, #242911, #8929, .T. ) ;
#182209=CARTESIAN_POINT ( 'NONE',  ( -16.87683809663752754, 61.18214872564366402, -220.4678436623806022 ) ) ;
#182225=CARTESIAN_POINT ( 'NONE',  ( 16.87683809663750267, 60.93935776605891164, -221.0417277355860790 ) ) ;
#182324=CARTESIAN_POINT ( 'NONE',  ( 15.74999999999999645, 62.10905854918434699, -217.1108499610991203 ) ) ;
#182338=ORIENTED_EDGE ( 'NONE', *, *, #32495, .T. ) ;
#182347=CARTESIAN_POINT ( 'NONE',  ( -16.89268316805466341, 60.93619025550653134, -221.0468289635910537 ) ) ;
#182356=AXIS2_PLACEMENT_3D ( 'NONE', #4739, #25621, #165128 ) ;
#182391=EDGE_CURVE ( 'NONE', #158643, #74054, #25619, .T. ) ;
#182406=AXIS2_PLACEMENT_3D ( 'NONE', #39598, #119105, #181651 ) ;
#182487=DIRECTION ( 'NONE',  ( 0.000000000000000000, 0.9651348961777157509, -0.2617529984165031243 ) ) ;
#182661=EDGE_CURVE ( 'NONE', #230787, #250736, #38449, .T. ) ;
#182947=CARTESIAN_POINT ( 'NONE',  ( -23.25000000000000355, 58.31215475832291162, -223.8520309854405923 ) ) ;
#183145=EDGE_CURVE ( 'NONE', #228089, #50473, #102903, .T. ) ;
#183208=CARTESIAN_POINT ( 'NONE',  ( -16.90137573187934805, 60.97558894184935241, -220.9081362493511449 ) ) ;
#183304=EDGE_LOOP ( 'NONE', ( #193262, #163006 ) ) ;
#183407=CARTESIAN_POINT ( 'NONE',  ( -16.92778301347321346, 63.05711598624363745, -213.0385060362119702 ) ) ;
#183413=FACE_OUTER_BOUND ( 'NONE', #125077, .T. ) ;
#183489=CARTESIAN_POINT ( 'NONE',  ( -16.77308656112213825, 60.93940833456625938, -221.0415412795326233 ) ) ;
#183523=DIRECTION ( 'NONE',  ( -1.073024830501117725E-15, 0.2617529984165031243, 0.9651348961777157509 ) ) ;
#183532=AXIS2_PLACEMENT_3D ( 'NONE', #104146, #183715, #5034 ) ;
#183715=DIRECTION ( 'NONE',  ( 1.000000000000000000, 0.000000000000000000, 0.000000000000000000 ) ) ;
#183969=EDGE_CURVE ( 'NONE', #243144, #96731, #232159, .T. ) ;
#184022=DIRECTION ( 'NONE',  ( -1.652117596168391700E-15, 0.9651348961777157509, -0.2617529984165031243 ) ) ;
#184054=CARTESIAN_POINT ( 'NONE',  ( 15.69410316191958010, 62.70378344720913333, -216.8024073824997799 ) ) ;
#184479=ORIENTED_EDGE ( 'NONE', *, *, #167346, .F. ) ;
#184793=FACE_OUTER_BOUND ( 'NONE', #152100, .T. ) ;
#184828=CARTESIAN_POINT ( 'NONE',  ( -15.39126916658602973, 62.83289218956783628, -216.2009511582250809 ) ) ;
#185329=ORIENTED_EDGE ( 'NONE', *, *, #74848, .T. ) ;
#185383=PLANE ( 'NONE',  #120162 ) ;
#185590=ORIENTED_EDGE ( 'NONE', *, *, #32495, .F. ) ;
#185591=STYLED_ITEM ( 'NONE', ( #62115 ), #51500 ) ;
#185599=ADVANCED_FACE ( 'NONE', ( #188767 ), #70141, .F. ) ;
#185988=EDGE_CURVE ( 'NONE', #198538, #83517, #137154, .T. ) ;
#186220=DIRECTION ( 'NONE',  ( 0.000000000000000000, -0.2617529984165152257, -0.9651348961777124202 ) ) ;
#186311=VECTOR ( 'NONE', #34217, 1000.000000000000000 ) ;
#186333=VECTOR ( 'NONE', #11422, 1000.000000000000000 ) ;
#186519=VERTEX_POINT ( 'NONE', #119884 ) ;
#186644=CARTESIAN_POINT ( 'NONE',  ( 15.39170923737819408, 62.83279349218705079, -216.2014764372738114 ) ) ;
#186956=EDGE_CURVE ( 'NONE', #22197, #5980, #138652, .T. ) ;
#187174=ORIENTED_EDGE ( 'NONE', *, *, #228054, .F. ) ;
#187236=ORIENTED_EDGE ( 'NONE', *, *, #82912, .F. ) ;
#187381=ORIENTED_EDGE ( 'NONE', *, *, #197823, .T. ) ;
#187699=CARTESIAN_POINT ( 'NONE',  ( -18.40000000000000213, 67.23581240663841641, -214.2531594801197627 ) ) ;
#187743=CARTESIAN_POINT ( 'NONE',  ( -16.87683809663752399, 61.03587125567668181, -221.0679030354277188 ) ) ;
#187748=CARTESIAN_POINT ( 'NONE',  ( -16.87036670365549895, 60.86740053880574663, -221.1564527318009254 ) ) ;
#187797=CARTESIAN_POINT ( 'NONE',  ( -12.25000000000000178, 62.59162599727320497, -217.2417264603073477 ) ) ;
#187852=CARTESIAN_POINT ( 'NONE',  ( -14.00000000000000178, 62.10905854918435409, -217.1108499610990918 ) ) ;
#188013=( BOUNDED_CURVE ( )  B_SPLINE_CURVE ( 3, ( #15228, #138971, #156030, #193857 ),
 .UNSPECIFIED., .F., .F. ) 
 B_SPLINE_CURVE_WITH_KNOTS ( ( 4, 4 ),
 ( 3.752122642744808445, 4.712388980384676351 ),
 .UNSPECIFIED. ) 
 CURVE ( )  GEOMETRIC_REPRESENTATION_ITEM ( )  RATIONAL_B_SPLINE_CURVE ( ( 1.000000000000000000, 0.9246222802177559430, 0.9246222802177559430, 1.000000000000000000 ) ) 
 REPRESENTATION_ITEM ( '' )  );
#188104=DIRECTION ( 'NONE',  ( -0.7071067811865456854, -0.6824534298470390503, 0.1850873201762214815 ) ) ;
#188487=DIRECTION ( 'NONE',  ( -1.000000000000000000, -0.000000000000000000, 0.000000000000000000 ) ) ;
#188495=CARTESIAN_POINT ( 'NONE',  ( -16.87683809663753465, 61.18526039135985428, -220.4600993141388301 ) ) ;
#188764=CARTESIAN_POINT ( 'NONE',  ( -23.25000000000000355, 65.08943781962308606, -222.1672656287770451 ) ) ;
#188767=FACE_OUTER_BOUND ( 'NONE', #37399, .T. ) ;
#188872=EDGE_CURVE ( 'NONE', #36086, #231042, #25058, .T. ) ;
#189561=ORIENTED_EDGE ( 'NONE', *, *, #256578, .F. ) ;
#189575=PLANE ( 'NONE',  #248062 ) ;
#189715=CARTESIAN_POINT ( 'NONE',  ( -16.88005004766534967, 63.08572333212228500, -213.1272708865124059 ) ) ;
#189767=CARTESIAN_POINT ( 'NONE',  ( 21.72449340488910607, 62.76341949586993962, -213.0402075299554951 ) ) ;
#189903=CARTESIAN_POINT ( 'NONE',  ( -18.40000000000000213, 58.56629890316250453, -223.9209570932885356 ) ) ;
#190262=EDGE_CURVE ( 'NONE', #198538, #168071, #78004, .T. ) ;
#190343=CARTESIAN_POINT ( 'NONE',  ( -18.40000000000000213, 65.08943781962308606, -222.1672656287770451 ) ) ;
#190552=CARTESIAN_POINT ( 'NONE',  ( -20.65000000000000568, 64.19947762500697763, -225.4487242757812737 ) ) ;
#190589=CARTESIAN_POINT ( 'NONE',  ( -18.39999999999999858, 58.59921997668411819, -223.8511959880075608 ) ) ;
#190843=ADVANCED_FACE ( 'NONE', ( #45300 ), #6151, .F. ) ;
#190876=ORIENTED_EDGE ( 'NONE', *, *, #209856, .F. ) ;
#190911=DIRECTION ( 'NONE',  ( 0.000000000000000000, 0.9651348961777379554, -0.2617529984164210233 ) ) ;
#191101=LINE ( 'NONE', #210639, #42741 ) ;
#191194=EDGE_CURVE ( 'NONE', #115941, #118873, #1427, .T. ) ;
#191205=DIRECTION ( 'NONE',  ( 0.8049926720990050466, -0.5725998182664976399, 0.1552940629517993720 ) ) ;
#191350=CARTESIAN_POINT ( 'NONE',  ( -16.94445028196808778, 60.88759175473954599, -221.0718995934454938 ) ) ;
#191424=EDGE_CURVE ( 'NONE', #168071, #137676, #151244, .T. ) ;
#191565=CARTESIAN_POINT ( 'NONE',  ( -16.93388492042258164, 60.88892937063719302, -221.0804221601966901 ) ) ;
#191795=CARTESIAN_POINT ( 'NONE',  ( 12.93279065517211102, 62.89055100415843924, -215.8809258249640379 ) ) ;
#191798=PLANE ( 'NONE',  #111731 ) ;
#192023=LINE ( 'NONE', #94171, #124335 ) ;
#192104=AXIS2_PLACEMENT_3D ( 'NONE', #253411, #74822, #190911 ) ;
#192220=FACE_OUTER_BOUND ( 'NONE', #240611, .T. ) ;
#192244=LINE ( 'NONE', #254719, #230509 ) ;
#192256=ORIENTED_EDGE ( 'NONE', *, *, #185988, .T. ) ;
#192296=LINE ( 'NONE', #153197, #225621 ) ;
#192480=DIRECTION ( 'NONE',  ( -0.7071067811865463515, 0.6824534298470381621, -0.1850873201762220366 ) ) ;
#192565=ORIENTED_EDGE ( 'NONE', *, *, #70889, .F. ) ;
#192784=AXIS2_PLACEMENT_3D ( 'NONE', #71385, #55609, #51776 ) ;
#192786=ORIENTED_EDGE ( 'NONE', *, *, #70889, .T. ) ;
#193100=ORIENTED_EDGE ( 'NONE', *, *, #126371, .T. ) ;
#193191=CARTESIAN_POINT ( 'NONE',  ( 12.25000000000000000, 62.10905854918434699, -217.1108499610991203 ) ) ;
#193241=CARTESIAN_POINT ( 'NONE',  ( -18.40000000000000213, 59.20211495293902004, -220.5705723384363921 ) ) ;
#193262=ORIENTED_EDGE ( 'NONE', *, *, #45816, .T. ) ;
#193653=AXIS2_PLACEMENT_3D ( 'NONE', #99188, #94067, #65213 ) ;
#193813=VECTOR ( 'NONE', #62883, 1000.000000000000114 ) ;
#193857=CARTESIAN_POINT ( 'NONE',  ( -17.11825945287481332, 62.98921886345645760, -213.1014462870871569 ) ) ;
#193992=CYLINDRICAL_SURFACE ( 'NONE', #73290, 0.1000000000000003525 ) ;
#194386=AXIS2_PLACEMENT_3D ( 'NONE', #142753, #39849, #119370 ) ;
#194505=EDGE_CURVE ( 'NONE', #102030, #25976, #251908, .T. ) ;
#194659=CARTESIAN_POINT ( 'NONE',  ( -16.88705144915396517, 63.01218536341742293, -213.3988038337647595 ) ) ;
#195053=ORIENTED_EDGE ( 'NONE', *, *, #152057, .T. ) ;
#195222=ORIENTED_EDGE ( 'NONE', *, *, #116562, .T. ) ;
#195242=CARTESIAN_POINT ( 'NONE',  ( -21.65000000000000213, 60.93935776605891164, -221.0417277355860790 ) ) ;
#195262=CARTESIAN_POINT ( 'NONE',  ( -16.94180778212363236, 60.88640190408171549, -221.0748371733828606 ) ) ;
#195340=ORIENTED_EDGE ( 'NONE', *, *, #126371, .F. ) ;
#195341=CARTESIAN_POINT ( 'NONE',  ( -16.87036670365548474, 63.08160062417908165, -212.9922606024214531 ) ) ;
#195430=ADVANCED_FACE ( 'NONE', ( #43585 ), #242032, .T. ) ;
#195616=CARTESIAN_POINT ( 'NONE',  ( -16.27683809663751191, 61.49226340392389289, -221.2952930242537377 ) ) ;
#195626=ORIENTED_EDGE ( 'NONE', *, *, #225353, .T. ) ;
#195712=CARTESIAN_POINT ( 'NONE',  ( -18.40000000000000213, 61.64185094745226934, -212.6324159020321076 ) ) ;
#195795=ADVANCED_FACE ( 'NONE', ( #244033 ), #43284, .F. ) ;
#195839=CARTESIAN_POINT ( 'NONE',  ( -16.92989507731676824, 63.02487450102639599, -213.3520164823955838 ) ) ;
#195976=CARTESIAN_POINT ( 'NONE',  ( -17.11825945287482753, 60.96553306590055854, -220.9452142459683159 ) ) ;
#196085=ORIENTED_EDGE ( 'NONE', *, *, #93336, .T. ) ;
#196194=CARTESIAN_POINT ( 'NONE',  ( -16.92563707711778420, 63.07545484833583771, -213.0929648075107536 ) ) ;
#196308=CARTESIAN_POINT ( 'NONE',  ( -16.77683809663752257, 48.78215419113038109, -213.4964773079645681 ) ) ;
#196439=CARTESIAN_POINT ( 'NONE',  ( -16.92925196614876882, 60.90909993422622648, -221.0679780288619156 ) ) ;
#196734=LINE ( 'NONE', #75534, #247525 ) ;
#196773=DIRECTION ( 'NONE',  ( 1.000000000000000000, 0.000000000000000000, 0.000000000000000000 ) ) ;
#196841=AXIS2_PLACEMENT_3D ( 'NONE', #216830, #156899, #60322 ) ;
#197185=CARTESIAN_POINT ( 'NONE',  ( -16.77180007708461318, 63.08949790057268103, -213.1137372711198452 ) ) ;
#197333=B_SPLINE_CURVE_WITH_KNOTS ( 'NONE', 3,
 ( #103635, #181919, #147933, #85347, #223585, #183208, #146616, #28008, #25424, #144051 ),
 .UNSPECIFIED., .F., .F.,
 ( 4, 2, 2, 2, 4 ),
 ( 0.000000000000000000, 0.0003916577441626488279, 0.0005874866162439766571, 0.0006854010522846775430, 0.0007833154883253782121 ),
 .UNSPECIFIED. ) ;
#197790=CARTESIAN_POINT ( 'NONE',  ( -16.93226657140833069, 60.87288173690708248, -221.0975609556742540 ) ) ;
#197823=EDGE_CURVE ( 'NONE', #174664, #14211, #39541, .T. ) ;
#197869=CARTESIAN_POINT ( 'NONE',  ( -15.75000000000000355, 62.59162599727320497, -217.2417264603073477 ) ) ;
#198303=SHAPE_REPRESENTATION ( 'Snap Open Cable Crossbars 10', ( #2425 ), #210534 ) ;
#198479=MANIFOLD_SOLID_BREP ( 'Stock-MAS-200-1', #207597 ) ;
#198538=VERTEX_POINT ( 'NONE', #246259 ) ;
#198656=EDGE_CURVE ( 'NONE', #50473, #229612, #230550, .T. ) ;
#198715=CARTESIAN_POINT ( 'NONE',  ( -16.93344882324368683, 63.05726507258725633, -213.0545985399865856 ) ) ;
#198798=B_SPLINE_CURVE_WITH_KNOTS ( 'NONE', 3,
 ( #115655, #53103, #230469, #235586, #174395, #251297, #16569 ),
 .UNSPECIFIED., .F., .F.,
 ( 4, 3, 4 ),
 ( 0.000000000000000000, 3.882884552234286342E-05, 5.798605692158378976E-05 ),
 .UNSPECIFIED. ) ;
#199112=CARTESIAN_POINT ( 'NONE',  ( -16.92570016628985385, 63.08493209837725146, -213.0969949883626100 ) ) ;
#199145=AXIS2_PLACEMENT_3D ( 'NONE', #225740, #87518, #62839 ) ;
#199203=CARTESIAN_POINT ( 'NONE',  ( -16.96982749440685367, 61.06363243814870145, -220.5835025252905268 ) ) ;
#199274=ORIENTED_EDGE ( 'NONE', *, *, #183145, .F. ) ;
#199538=DIRECTION ( 'NONE',  ( 1.000000000000000000, -1.145314911736513911E-16, 3.106193895438251633E-17 ) ) ;
#199544=DIRECTION ( 'NONE',  ( 0.000000000000000000, 0.2617529984165031243, 0.9651348961777157509 ) ) ;
#199550=ORIENTED_EDGE ( 'NONE', *, *, #17385, .T. ) ;
#199565=CARTESIAN_POINT ( 'NONE',  ( -16.89268316805465986, 63.08557629953710943, -213.1216189793661329 ) ) ;
#199600=DIRECTION ( 'NONE',  ( 1.186688945009009831E-16, 0.9651348961777157509, -0.2617529984165031243 ) ) ;
#200009=LINE ( 'NONE', #38367, #23763 ) ;
#200011=CARTESIAN_POINT ( 'NONE',  ( -16.93860193097148326, 63.05725141050672278, -213.0679477116501062 ) ) ;
#200186=CARTESIAN_POINT ( 'NONE',  ( -18.40000000000000213, 61.75216633358002127, -212.7659468556851436 ) ) ;
#200261=( BOUNDED_CURVE ( )  B_SPLINE_CURVE ( 3, ( #3240, #59344, #181906, #200186 ),
 .UNSPECIFIED., .F., .T. ) 
 B_SPLINE_CURVE_WITH_KNOTS ( ( 4, 4 ),
 ( -1.172395514004165307E-13, 1.570796326794935194 ),
 .UNSPECIFIED. ) 
 CURVE ( )  GEOMETRIC_REPRESENTATION_ITEM ( )  RATIONAL_B_SPLINE_CURVE ( ( 1.000000000000000000, 0.8047378541243281891, 0.8047378541243281891, 1.000000000000000000 ) ) 
 REPRESENTATION_ITEM ( '' )  );
#200373=CARTESIAN_POINT ( 'NONE',  ( -16.93339986808596365, 60.86418613339449024, -221.1083815558925778 ) ) ;
#200399=CARTESIAN_POINT ( 'NONE',  ( -16.85718274719333465, 63.08318335034096691, -213.0371462789988186 ) ) ;
#200484=CARTESIAN_POINT ( 'NONE',  ( -16.82542659449988065, 60.97908861380064138, -220.9544488154746773 ) ) ;
#200542=CARTESIAN_POINT ( 'NONE',  ( -18.40000000000000213, 59.44312576075365229, -220.7395490299249445 ) ) ;
#200557=FACE_OUTER_BOUND ( 'NONE', #180784, .T. ) ;
#200653=ORIENTED_EDGE ( 'NONE', *, *, #188872, .F. ) ;
#200828=CARTESIAN_POINT ( 'NONE',  ( 18.54999999999999716, 64.24389422848744857, -213.4417251850286164 ) ) ;
#200880=ORIENTED_EDGE ( 'NONE', *, *, #179217, .T. ) ;
#200974=CARTESIAN_POINT ( 'NONE',  ( -17.11825945287482753, 60.84284427644114146, -221.0155524357444108 ) ) ;
#201095=DIRECTION ( 'NONE',  ( -1.000000000000000000, 1.589006537307804524E-14, -4.309524267446607808E-15 ) ) ;
#201328=CARTESIAN_POINT ( 'NONE',  ( -16.93935632781549572, 63.06259405572221510, -213.0802528019004001 ) ) ;
#201365=CARTESIAN_POINT ( 'NONE',  ( -16.92209698673656249, 63.06986081158819246, -213.1861430886383459 ) ) ;
#201540=CARTESIAN_POINT ( 'NONE',  ( -20.65000000000000568, 62.65526179112262639, -225.0299194783148948 ) ) ;
#201734=DIRECTION ( 'NONE',  ( -1.000000000000000000, -0.000000000000000000, 0.000000000000000000 ) ) ;
#202127=CYLINDRICAL_SURFACE ( 'NONE', #224910, 0.9000000000000014655 ) ;
#202217=ORIENTED_EDGE ( 'NONE', *, *, #135235, .T. ) ;
#202379=CARTESIAN_POINT ( 'NONE',  ( 12.25000000000000000, 62.59162599727320497, -217.2417264603073761 ) ) ;
#202871=CARTESIAN_POINT ( 'NONE',  ( -16.27683809663751191, 60.62847850914942427, -224.4802381816402601 ) ) ;
#202959=VECTOR ( 'NONE', #119541, 1000.000000000000000 ) ;
#203002=ORIENTED_EDGE ( 'NONE', *, *, #48487, .T. ) ;
#203035=CARTESIAN_POINT ( 'NONE',  ( -16.82055514392408213, 60.94637224242198670, -221.0158639786953358 ) ) ;
#203039=DIRECTION ( 'NONE',  ( 1.000000000000000000, 2.670994536826046953E-16, 9.848483305199541222E-16 ) ) ;
#203114=CARTESIAN_POINT ( 'NONE',  ( -15.75000000000000355, 62.59162599727320497, -217.2417264603073477 ) ) ;
#203438=CIRCLE ( 'NONE', #41134, 0.1999999999999987899 ) ;
#203554=FACE_OUTER_BOUND ( 'NONE', #220787, .T. ) ;
#203833=ORIENTED_EDGE ( 'NONE', *, *, #33245, .T. ) ;
#203849=CARTESIAN_POINT ( 'NONE',  ( -16.93826681692523550, 63.05143189155258909, -213.0194121372203995 ) ) ;
#204057=ORIENTED_EDGE ( 'NONE', *, *, #153853, .T. ) ;
#204066=FACE_OUTER_BOUND ( 'NONE', #3778, .T. ) ;
#204241=PLANE ( 'NONE',  #182356 ) ;
#204538=CARTESIAN_POINT ( 'NONE',  ( -23.25000000000000355, 61.34848953995435039, -212.6564661897791098 ) ) ;
#204890=CARTESIAN_POINT ( 'NONE',  ( 15.74999999999999645, 62.62192211835341027, -217.1300186905771170 ) ) ;
#204926=CARTESIAN_POINT ( 'NONE',  ( 15.52844286134408769, 62.33593033127508676, -218.0864590324956964 ) ) ;
#205367=VERTEX_POINT ( 'NONE', #158418 ) ;
#205386=CARTESIAN_POINT ( 'NONE',  ( -16.86379686415369861, 60.89319167309326275, -221.1156094034376451 ) ) ;
#205601=PLANE ( 'NONE',  #170755 ) ;
#205723=ORIENTED_EDGE ( 'NONE', *, *, #162852, .T. ) ;
#205766=CARTESIAN_POINT ( 'NONE',  ( -23.25000000000000355, 62.96304356361481780, -213.1979597767049484 ) ) ;
#205841=SURFACE_SIDE_STYLE ('',( #65043 ) ) ;
#205972=DIRECTION ( 'NONE',  ( -1.000000000000000000, 0.000000000000000000, 0.000000000000000000 ) ) ;
#206156=ORIENTED_EDGE ( 'NONE', *, *, #7570, .F. ) ;
#206664=CYLINDRICAL_SURFACE ( 'NONE', #90465, 0.09999999999999911737 ) ;
#206781=CARTESIAN_POINT ( 'NONE',  ( -16.80468759584940486, 60.95740558621518090, -221.0051579303695917 ) ) ;
#206821=EDGE_CURVE ( 'NONE', #91602, #228089, #120328, .T. ) ;
#206880=ORIENTED_EDGE ( 'NONE', *, *, #145008, .F. ) ;
#207030=CARTESIAN_POINT ( 'NONE',  ( -21.65000000000000213, 63.05955705323258798, -213.2241350765465882 ) ) ;
#207070=CARTESIAN_POINT ( 'NONE',  ( -16.77732147262506146, 63.08608884956520768, -213.1417150269271303 ) ) ;
#207158=ADVANCED_FACE ( 'NONE', ( #20904 ), #154021, .F. ) ;
#207313=ORIENTED_EDGE ( 'NONE', *, *, #182391, .F. ) ;
#207344=VECTOR ( 'NONE', #105924, 1000.000000000000000 ) ;
#207359=CARTESIAN_POINT ( 'NONE',  ( -12.84409460144754078, 62.18784473894375964, -218.4987171750604773 ) ) ;
#207597=CLOSED_SHELL ( 'NONE', ( #131433, #71555, #95605, #16428, #211587, #195795, #77335, #190843, #160075, #83431, #80503, #83455, #9041, #243092, #98261, #119910, #181955, #11295, #185599, #251865, #17065, #214277, #148683, #84015, #51445, #41666, #33220, #27957, #131560, #68807, #91736, #107053, #233685, #25315, #130884, #62177, #40383, #207158, #95347, #41332, #175133, #7636, #25348, #149248, #219880, #34917, #41348, #36003, #41894, #154871, #120909, #195430, #111728 ) ) ;
#207727=CARTESIAN_POINT ( 'NONE',  ( -16.77683809663752257, 60.94702803318471496, -221.0293550571836647 ) ) ;
#207932=EDGE_LOOP ( 'NONE', ( #212205, #220781, #214047, #149837, #52591 ) ) ;
#207979=ORIENTED_EDGE ( 'NONE', *, *, #138189, .F. ) ;
#208001=ORIENTED_EDGE ( 'NONE', *, *, #48487, .F. ) ;
#208121=CARTESIAN_POINT ( 'NONE',  ( 23.04999999999999716, 65.06382255409391746, -210.1412732845728897 ) ) ;
#208136=AXIS2_PLACEMENT_3D ( 'NONE', #2094, #141617, #106319 ) ;
#208240=DIRECTION ( 'NONE',  ( 0.000000000000000000, 0.2617529984165031243, 0.9651348961777157509 ) ) ;
#208270=CARTESIAN_POINT ( 'NONE',  ( -12.42749937872396160, 62.77489950700472576, -216.4869172218852214 ) ) ;
#208308=DIRECTION ( 'NONE',  ( -0.5932847527679298016, -0.7769265190100954621, 0.2107092456252268875 ) ) ;
#208342=DIRECTION ( 'NONE',  ( -1.000000000000000000, 0.000000000000000000, 0.000000000000000000 ) ) ;
#208899=ORIENTED_EDGE ( 'NONE', *, *, #253038, .T. ) ;
#209093=VERTEX_POINT ( 'NONE', #11417 ) ;
#209223=FACE_OUTER_BOUND ( 'NONE', #207932, .T. ) ;
#209336=CARTESIAN_POINT ( 'NONE',  ( -16.85939591225059431, 61.06373154741859111, -220.7541896542538780 ) ) ;
#209505=VECTOR ( 'NONE', #212651, 1000.000000000000000 ) ;
#209751=CARTESIAN_POINT ( 'NONE',  ( 12.25000000000000000, 62.10905854918434699, -217.1108499610991203 ) ) ;
#209838=LINE ( 'NONE', #31241, #26405 ) ;
#209856=EDGE_CURVE ( 'NONE', #66925, #110195, #151566, .T. ) ;
#209864=AXIS2_PLACEMENT_3D ( 'NONE', #33700, #151040, #212305 ) ;
#209928=CARTESIAN_POINT ( 'NONE',  ( -14.11697426661281973, 62.02991417940919661, -218.9025163457276335 ) ) ;
#210018=EDGE_CURVE ( 'NONE', #31477, #27216, #143339, .T. ) ;
#210534=( GEOMETRIC_REPRESENTATION_CONTEXT ( 3 ) GLOBAL_UNCERTAINTY_ASSIGNED_CONTEXT ( ( #74137 ) ) GLOBAL_UNIT_ASSIGNED_CONTEXT ( ( #63371, #242020, #144189 ) ) REPRESENTATION_CONTEXT ( 'NONE', 'WORKASPACE' ) );
#210545=CARTESIAN_POINT ( 'NONE',  ( -17.29838795459677314, 60.20407299469992068, -222.1423803938182289 ) ) ;
#210592=DIRECTION ( 'NONE',  ( -0.000000000000000000, 0.2617529984165031243, 0.9651348961777157509 ) ) ;
#210606=CIRCLE ( 'NONE', #60572, 1.500000000000001332 ) ;
#210639=CARTESIAN_POINT ( 'NONE',  ( 18.39999999999999503, 61.34848953995435039, -212.6564661897791098 ) ) ;
#210701=EDGE_CURVE ( 'NONE', #172111, #39830, #119201, .T. ) ;
#211102=CARTESIAN_POINT ( 'NONE',  ( -16.97092634996741722, 60.88504535834231035, -221.0475723052460069 ) ) ;
#211126=ORIENTED_EDGE ( 'NONE', *, *, #157312, .F. ) ;
#211232=CARTESIAN_POINT ( 'NONE',  ( -16.78569801330229438, 60.94316146603833317, -221.0355967009543292 ) ) ;
#211363=LINE ( 'NONE', #112272, #209505 ) ;
#211496=DIRECTION ( 'NONE',  ( 1.000000000000000000, 0.000000000000000000, 0.000000000000000000 ) ) ;
#211587=ADVANCED_FACE ( 'NONE', ( #128564 ), #225069, .F. ) ;
#211630=EDGE_LOOP ( 'NONE', ( #212708, #20213, #192256, #106581 ) ) ;
#211757=VERTEX_POINT ( 'NONE', #214506 ) ;
#211762=LINE ( 'NONE', #173964, #81880 ) ;
#211858=CARTESIAN_POINT ( 'NONE',  ( 18.54999999999999716, 64.24389422848744857, -213.4417251850286164 ) ) ;
#212205=ORIENTED_EDGE ( 'NONE', *, *, #34136, .F. ) ;
#212305=DIRECTION ( 'NONE',  ( 1.000000000000000000, 0.000000000000000000, 0.000000000000000000 ) ) ;
#212345=ORIENTED_EDGE ( 'NONE', *, *, #84935, .F. ) ;
#212502=AXIS2_PLACEMENT_3D ( 'NONE', #217953, #161884, #238830 ) ;
#212536=CARTESIAN_POINT ( 'NONE',  ( -16.80438519320023261, 60.93976421501079699, -221.0410730170675606 ) ) ;
#212624=CARTESIAN_POINT ( 'NONE',  ( 12.30626653967341078, 62.70412490954448259, -216.8009802157223191 ) ) ;
#212651=DIRECTION ( 'NONE',  ( 1.000000000000000000, 0.000000000000000000, 0.000000000000000000 ) ) ;
#212708=ORIENTED_EDGE ( 'NONE', *, *, #191194, .F. ) ;
#212799=DIRECTION ( 'NONE',  ( -0.000000000000000000, 0.2617529984165031243, 0.9651348961777157509 ) ) ;
#212928=CARTESIAN_POINT ( 'NONE',  ( -14.87779219673427811, 62.11640146696787923, -218.6859212199907745 ) ) ;
#213427=ORIENTED_EDGE ( 'NONE', *, *, #173115, .T. ) ;
#213826=VECTOR ( 'NONE', #151647, 1000.000000000000000 ) ;
#214047=ORIENTED_EDGE ( 'NONE', *, *, #186956, .T. ) ;
#214132=CARTESIAN_POINT ( 'NONE',  ( 13.99999999999999822, 62.10905854918434699, -217.1108499610991203 ) ) ;
#214197=CARTESIAN_POINT ( 'NONE',  ( -16.85697194749134553, 63.05114253962987192, -213.4135404582943067 ) ) ;
#214277=ADVANCED_FACE ( 'NONE', ( #22579 ), #21312, .T. ) ;
#214296=CARTESIAN_POINT ( 'NONE',  ( -20.65000000000000568, 65.08943781962308606, -222.1672656287770451 ) ) ;
#214301=DIRECTION ( 'NONE',  ( 1.000000000000000000, -1.145314911736513664E-16, 3.106193895438251016E-17 ) ) ;
#214359=DIRECTION ( 'NONE',  ( 0.000000000000000000, -0.9651348961777157509, 0.2617529984165031243 ) ) ;
#214460=CARTESIAN_POINT ( 'NONE',  ( -16.94445028196807002, 63.05630424923659660, -213.0754291771441729 ) ) ;
#214482=EDGE_CURVE ( 'NONE', #222464, #137276, #26432, .T. ) ;
#214506=CARTESIAN_POINT ( 'NONE',  ( 23.24999999999999645, 64.17386235947780904, -213.4227319315771183 ) ) ;
#214624=ORIENTED_EDGE ( 'NONE', *, *, #249196, .F. ) ;
#214759=ORIENTED_EDGE ( 'NONE', *, *, #233839, .F. ) ;
#214810=LINE ( 'NONE', #101233, #162688 ) ;
#214812=CARTESIAN_POINT ( 'NONE',  ( -15.55912972643740488, 64.52016466995087285, -213.4130396782846901 ) ) ;
#215037=ORIENTED_EDGE ( 'NONE', *, *, #26508, .T. ) ;
#215556=VECTOR ( 'NONE', #85077, 1000.000000000000000 ) ;
#215717=ORIENTED_EDGE ( 'NONE', *, *, #171046, .T. ) ;
#215867=LINE ( 'NONE', #170402, #56759 ) ;
#215994=CARTESIAN_POINT ( 'NONE',  ( -16.91247567987036859, 60.92502281432796707, -221.0598840834026930 ) ) ;
#216176=CARTESIAN_POINT ( 'NONE',  ( -17.11825945287481332, 62.96304356361481780, -213.1979597767049484 ) ) ;
#216358=CARTESIAN_POINT ( 'NONE',  ( -16.81095280782811230, 60.93935776605868426, -221.0417277355869317 ) ) ;
#216379=CYLINDRICAL_SURFACE ( 'NONE', #244647, 0.09999999999999939493 ) ;
#216622=EDGE_LOOP ( 'NONE', ( #218864, #189561, #102804, #245049 ) ) ;
#216796=CARTESIAN_POINT ( 'NONE',  ( 12.47034474403012716, 62.33660315667518148, -218.0844802857457978 ) ) ;
#216830=CARTESIAN_POINT ( 'NONE',  ( -21.64999999999999858, 62.96304356361481780, -213.1979597767049484 ) ) ;
#216884=VECTOR ( 'NONE', #94123, 1000.000000000000000 ) ;
#217230=LINE ( 'NONE', #22933, #93199 ) ;
#217236=CARTESIAN_POINT ( 'NONE',  ( -16.80100914604134132, 63.08371810292741344, -213.1612216948777530 ) ) ;
#217467=CYLINDRICAL_SURFACE ( 'NONE', #226971, 1.500000000000001332 ) ;
#217472=EDGE_CURVE ( 'NONE', #96731, #179633, #27024, .T. ) ;
#217783=ORIENTED_EDGE ( 'NONE', *, *, #58822, .F. ) ;
#217953=CARTESIAN_POINT ( 'NONE',  ( -18.40000000000000213, 68.12577260125452483, -210.9717008331155341 ) ) ;
#218016=CARTESIAN_POINT ( 'NONE',  ( -16.93710578446435377, 63.01537210432839231, -213.3870536919253595 ) ) ;
#218114=CARTESIAN_POINT ( 'NONE',  ( 23.24999999999999645, 58.31215475832291162, -223.8520309854405923 ) ) ;
#218303=DIRECTION ( 'NONE',  ( 1.000000000000000000, 0.000000000000000000, 0.000000000000000000 ) ) ;
#218391=EDGE_CURVE ( 'NONE', #7786, #249995, #71407, .T. ) ;
#218628=ORIENTED_EDGE ( 'NONE', *, *, #225965, .T. ) ;
#218755=EDGE_LOOP ( 'NONE', ( #252864, #118419, #113347, #207979 ) ) ;
#218864=ORIENTED_EDGE ( 'NONE', *, *, #2422, .T. ) ;
#218986=CARTESIAN_POINT ( 'NONE',  ( -21.64999999999999858, 60.84284427644114146, -221.0155524357444108 ) ) ;
#219175=ORIENTED_EDGE ( 'NONE', *, *, #174616, .F. ) ;
#219315=CARTESIAN_POINT ( 'NONE',  ( -16.89155683852818157, 62.92151589033651504, -213.7331200518002845 ) ) ;
#219320=CARTESIAN_POINT ( 'NONE',  ( -18.35235881385853318, 58.57909272559864178, -223.9244268894767629 ) ) ;
#219401=PLANE ( 'NONE',  #4166 ) ;
#219470=LINE ( 'NONE', #182947, #135545 ) ;
#219622=PRODUCT_DEFINITION_FORMATION_WITH_SPECIFIED_SOURCE ( 'ANY', '', #130599, .NOT_KNOWN. ) ;
#219697=EDGE_CURVE ( 'NONE', #124122, #6716, #229264, .T. ) ;
#219875=CARTESIAN_POINT ( 'NONE',  ( -23.25000000000000355, 64.19947762500697763, -225.4487242757812737 ) ) ;
#219880=ADVANCED_FACE ( 'NONE', ( #114440 ), #193992, .F. ) ;
#219983=VECTOR ( 'NONE', #220637, 1000.000000000000000 ) ;
#220209=ORIENTED_EDGE ( 'NONE', *, *, #59660, .T. ) ;
#220502=DIRECTION ( 'NONE',  ( -0.000000000000000000, 0.2617529984165031243, 0.9651348961777157509 ) ) ;
#220637=DIRECTION ( 'NONE',  ( 0.000000000000000000, 0.9651348961777157509, -0.2617529984165031243 ) ) ;
#220663=AXIS2_PLACEMENT_3D ( 'NONE', #218114, #61632, #177755 ) ;
#220664=CARTESIAN_POINT ( 'NONE',  ( 13.54556439290364622, 62.05118075326792848, -218.8501529344108292 ) ) ;
#220781=ORIENTED_EDGE ( 'NONE', *, *, #83550, .T. ) ;
#220787=EDGE_LOOP ( 'NONE', ( #231502, #16235, #222230, #203833, #245172, #21270 ) ) ;
#221010=PLANE ( 'NONE',  #194386 ) ;
#221031=LINE ( 'NONE', #64534, #44344 ) ;
#221090=DIRECTION ( 'NONE',  ( -1.000000000000000000, 0.000000000000000000, 0.000000000000000000 ) ) ;
#221104=CARTESIAN_POINT ( 'NONE',  ( -16.87368910959167678, 60.91865946774127849, -221.0749760015432344 ) ) ;
#221126=ORIENTED_EDGE ( 'NONE', *, *, #224797, .T. ) ;
#221145=DIRECTION ( 'NONE',  ( 1.000000000000000000, 0.000000000000000000, 0.000000000000000000 ) ) ;
#221280=CARTESIAN_POINT ( 'NONE',  ( -18.40000000000000213, 65.08943781962308606, -222.1672656287770451 ) ) ;
#221322=EDGE_LOOP ( 'NONE', ( #49563, #76089, #81889, #142799, #255750 ) ) ;
#221569=ORIENTED_EDGE ( 'NONE', *, *, #35781, .F. ) ;
#221738=CARTESIAN_POINT ( 'NONE',  ( -21.65000000000000213, 65.69159657275406516, -213.8343546826533839 ) ) ;
#222105=CARTESIAN_POINT ( 'NONE',  ( -16.93658211146644987, 63.05737344118514187, -213.0636739456002147 ) ) ;
#222230=ORIENTED_EDGE ( 'NONE', *, *, #214482, .T. ) ;
#222440=DIRECTION ( 'NONE',  ( 1.000000000000000000, 0.000000000000000000, 0.000000000000000000 ) ) ;
#222464=VERTEX_POINT ( 'NONE', #107781 ) ;
#222582=CARTESIAN_POINT ( 'NONE',  ( -16.85722902420167557, 60.96960266377776350, -220.9302088364852068 ) ) ;
#222741=ORIENTED_EDGE ( 'NONE', *, *, #191424, .T. ) ;
#222928=ORIENTED_EDGE ( 'NONE', *, *, #129149, .F. ) ;
#222985=CARTESIAN_POINT ( 'NONE',  ( 20.04999999999999716, 64.24389422848746278, -213.4417251850286164 ) ) ;
#223016=( BOUNDED_CURVE ( )  B_SPLINE_CURVE ( 3, ( #155589, #235094, #116432, #195976 ),
 .UNSPECIFIED., .F., .F. ) 
 B_SPLINE_CURVE_WITH_KNOTS ( ( 4, 4 ),
 ( 0.5235987755982174363, 1.570796326794896558 ),
 .UNSPECIFIED. ) 
 CURVE ( )  GEOMETRIC_REPRESENTATION_ITEM ( )  RATIONAL_B_SPLINE_CURVE ( ( 1.000000000000000000, 0.9106836025229455567, 0.9106836025229455567, 1.000000000000000000 ) ) 
 REPRESENTATION_ITEM ( '' )  );
#223402=CARTESIAN_POINT ( 'NONE',  ( -16.93294127766158752, 63.05522583286660421, -213.0365540695144944 ) ) ;
#223585=CARTESIAN_POINT ( 'NONE',  ( -16.92989143108098915, 61.00021111735996016, -220.8173494352598425 ) ) ;
#223707=FACE_OUTER_BOUND ( 'NONE', #256376, .T. ) ;
#223988=DIRECTION ( 'NONE',  ( 1.186688945009010077E-16, 0.9651348961777157509, -0.2617529984165031243 ) ) ;
#224130=PRODUCT_DEFINITION_SHAPE ( 'NONE', 'NONE',  #94639 ) ;
#224155=CYLINDRICAL_SURFACE ( 'NONE', #99426, 0.9000000000000014655 ) ;
#224576=( BOUNDED_CURVE ( )  B_SPLINE_CURVE ( 3, ( #91524, #8138, #90209, #171104 ),
 .UNSPECIFIED., .F., .F. ) 
 B_SPLINE_CURVE_WITH_KNOTS ( ( 4, 4 ),
 ( 3.432212674861198742, 3.693332928900582957 ),
 .UNSPECIFIED. ) 
 CURVE ( )  GEOMETRIC_REPRESENTATION_ITEM ( )  RATIONAL_B_SPLINE_CURVE ( ( 1.000000000000000000, 0.9943260843901261525, 0.9943260843901261525, 1.000000000000000000 ) ) 
 REPRESENTATION_ITEM ( '' )  );
#224783=EDGE_CURVE ( 'NONE', #166275, #102030, #256651, .T. ) ;
#224797=EDGE_CURVE ( 'NONE', #27216, #24894, #105296, .T. ) ;
#224840=ORIENTED_EDGE ( 'NONE', *, *, #105959, .T. ) ;
#224910=AXIS2_PLACEMENT_3D ( 'NONE', #103005, #181297, #205972 ) ;
#225069=PLANE ( 'NONE',  #102337 ) ;
#225210=ORIENTED_EDGE ( 'NONE', *, *, #82912, .T. ) ;
#225246=CARTESIAN_POINT ( 'NONE',  ( -17.11825945287481332, 62.98921886345645760, -213.1014462870871569 ) ) ;
#225353=EDGE_CURVE ( 'NONE', #250736, #163271, #53717, .T. ) ;
#225621=VECTOR ( 'NONE', #230124, 1000.000000000000000 ) ;
#225727=CARTESIAN_POINT ( 'NONE',  ( 15.66039659514494709, 62.72902952540357546, -216.6940264888114882 ) ) ;
#225740=CARTESIAN_POINT ( 'NONE',  ( 20.04999999999999716, 62.09751964147213954, -221.3558313336858703 ) ) ;
#225965=EDGE_CURVE ( 'NONE', #77430, #163271, #128809, .T. ) ;
#226209=CARTESIAN_POINT ( 'NONE',  ( -16.91256925476570316, 60.87407910423024049, -221.1459158692213407 ) ) ;
#226485=DIRECTION ( 'NONE',  ( -0.7071067811865462405, -0.6824534298470383842, 0.1850873201762212872 ) ) ;
#226505=CARTESIAN_POINT ( 'NONE',  ( -13.11924609551135568, 62.91308081279556319, -215.7443727990306002 ) ) ;
#226576=ORIENTED_EDGE ( 'NONE', *, *, #182661, .F. ) ;
#226677=( LENGTH_UNIT ( ) NAMED_UNIT ( * ) SI_UNIT ( .MILLI., .METRE. ) );
#226756=CARTESIAN_POINT ( 'NONE',  ( 13.99999999999999822, 62.10905854918434699, -217.1108499610991203 ) ) ;
#226916=( BOUNDED_SURFACE ( )  B_SPLINE_SURFACE ( 3, 2, ( 
 ( #146683, #171454, #151882 ),
 ( #128437, #29379, #248385 ),
 ( #210545, #69765, #231401 ),
 ( #52738, #226209, #47595 ) ),
 .UNSPECIFIED., .F., .F., .T. ) 
 B_SPLINE_SURFACE_WITH_KNOTS ( ( 4, 4 ),
 ( 3, 3 ),
 ( 5.727910411845712702, 5.983100554402350113 ),
 ( 0.000000000000000000, 1.000000000000000000 ),
 .UNSPECIFIED. ) 
 GEOMETRIC_REPRESENTATION_ITEM ( )  RATIONAL_B_SPLINE_SURFACE ( (
 ( 1.000000000000000000, 0.8946697475932056109, 1.000000000000000000),
 ( 1.000000000000000000, 0.9035312726220235957, 1.000000000000000000),
 ( 1.000000000000000000, 0.9104333467450250739, 1.000000000000000000),
 ( 1.000000000000000000, 0.9152888060719243102, 1.000000000000000000) ) ) 
 REPRESENTATION_ITEM ( '' )  SURFACE ( )  );
#226971=AXIS2_PLACEMENT_3D ( 'NONE', #234475, #76683, #237053 ) ;
#227315=B_SPLINE_CURVE_WITH_KNOTS ( 'NONE', 3,
 ( #21056, #77141, #254468, #257018, #100526, #195839, #58839, #57565, #238798, #156721 ),
 .UNSPECIFIED., .F., .F.,
 ( 4, 2, 2, 2, 4 ),
 ( 5.201972647453647240E-16, 9.930191194500248098E-05, 0.0001986038238894847617, 0.0003972076477784387523, 0.0007944152955563468961 ),
 .UNSPECIFIED. ) ;
#227397=DIRECTION ( 'NONE',  ( 0.000000000000000000, -0.2617529984165031243, -0.9651348961777157509 ) ) ;
#227614=CARTESIAN_POINT ( 'NONE',  ( -16.87372386987899375, 61.13702328834270361, -220.5780305565725996 ) ) ;
#227699=CARTESIAN_POINT ( 'NONE',  ( -16.97683809663752186, 61.23280479334029991, -220.3417702668378126 ) ) ;
#227807=CARTESIAN_POINT ( 'NONE',  ( -14.22969084473441015, 62.94440715787349916, -215.5359628679901789 ) ) ;
#228054=EDGE_CURVE ( 'NONE', #228089, #145413, #219470, .T. ) ;
#228089=VERTEX_POINT ( 'NONE', #26436 ) ;
#228178=CARTESIAN_POINT ( 'NONE',  ( 18.54999999999999716, 62.09751964147213954, -221.3558313336858987 ) ) ;
#228201=CARTESIAN_POINT ( 'NONE',  ( -13.22483237240078680, 62.09620004573545771, -218.7373296619003042 ) ) ;
#228932=DIRECTION ( 'NONE',  ( 0.000000000000000000, -0.9651348961777157509, 0.2617529984165031243 ) ) ;
#229085=ORIENTED_EDGE ( 'NONE', *, *, #51871, .T. ) ;
#229196=DIRECTION ( 'NONE',  ( 0.000000000000000000, 0.2617529984165031243, 0.9651348961777157509 ) ) ;
#229264=LINE ( 'NONE', #247533, #77162 ) ;
#229270=DIRECTION ( 'NONE',  ( 1.020425574104004196E-15, 0.2617529984165031243, 0.9651348961777157509 ) ) ;
#229612=VERTEX_POINT ( 'NONE', #143530 ) ;
#229754=CARTESIAN_POINT ( 'NONE',  ( 22.88900146558018989, 61.25204754149966391, -224.6493555398289459 ) ) ;
#229778=VECTOR ( 'NONE', #86449, 1000.000000000000000 ) ;
#229785=EDGE_LOOP ( 'NONE', ( #117610, #254602, #90221, #204057 ) ) ;
#230124=DIRECTION ( 'NONE',  ( 1.000000000000000000, -1.617093283983707315E-14, 3.273910559064800547E-15 ) ) ;
#230469=CARTESIAN_POINT ( 'NONE',  ( -18.36973785203556275, 62.50337617467221918, -209.4468579031038473 ) ) ;
#230509=VECTOR ( 'NONE', #214359, 1000.000000000000000 ) ;
#230526=VERTEX_POINT ( 'NONE', #207727 ) ;
#230550=LINE ( 'NONE', #231845, #35204 ) ;
#230554=AXIS2_PLACEMENT_3D ( 'NONE', #226756, #127671, #28619 ) ;
#230787=VERTEX_POINT ( 'NONE', #45761 ) ;
#231042=VERTEX_POINT ( 'NONE', #221738 ) ;
#231257=ORIENTED_EDGE ( 'NONE', *, *, #232902, .T. ) ;
#231401=CARTESIAN_POINT ( 'NONE',  ( -17.22767730082754767, 60.21573615951074743, -222.1845923959672291 ) ) ;
#231502=ORIENTED_EDGE ( 'NONE', *, *, #148382, .F. ) ;
#231765=DIRECTION ( 'NONE',  ( 1.000000000000000000, 0.000000000000000000, -0.000000000000000000 ) ) ;
#231845=CARTESIAN_POINT ( 'NONE',  ( 18.39999999999999503, 59.46930106059529209, -220.6430355403071530 ) ) ;
#232159=( BOUNDED_CURVE ( )  B_SPLINE_CURVE ( 3, ( #235854, #138027, #55915, #57201 ),
 .UNSPECIFIED., .F., .F. ) 
 B_SPLINE_CURVE_WITH_KNOTS ( ( 4, 4 ),
 ( 5.731445031868800832, 5.983100554402348337 ),
 .UNSPECIFIED. ) 
 CURVE ( )  GEOMETRIC_REPRESENTATION_ITEM ( )  RATIONAL_B_SPLINE_CURVE ( ( 1.000000000000000000, 0.9947294176030465618, 0.9947294176030465618, 1.000000000000000000 ) ) 
 REPRESENTATION_ITEM ( '' )  );
#232197=ORIENTED_EDGE ( 'NONE', *, *, #105533, .F. ) ;
#232512=CARTESIAN_POINT ( 'NONE',  ( -15.52965525596987462, 62.33660315667519569, -218.0844802857458262 ) ) ;
#232709=CARTESIAN_POINT ( 'NONE',  ( -16.87665923198281348, 63.08573235307424198, -213.1276215869287967 ) ) ;
#232761=DIRECTION ( 'NONE',  ( 0.5932847527679299127, 0.7769265190100951290, -0.2107092456252281365 ) ) ;
#232770=EDGE_CURVE ( 'NONE', #137676, #257876, #79090, .T. ) ;
#232902=EDGE_CURVE ( 'NONE', #25976, #21828, #167660, .T. ) ;
#233186=CARTESIAN_POINT ( 'NONE',  ( -17.71734398241074615, 62.84618681140459273, -210.6017155954972964 ) ) ;
#233259=CARTESIAN_POINT ( 'NONE',  ( -17.11825945287483108, 60.93935776605891874, -221.0417277355861074 ) ) ;
#233300=CARTESIAN_POINT ( 'NONE',  ( -18.40000000000000213, 61.75216633358002127, -212.7659468556851436 ) ) ;
#233575=LINE ( 'NONE', #134436, #134623 ) ;
#233685=ADVANCED_FACE ( 'NONE', ( #87152, #24661, #165437 ), #166744, .T. ) ;
#233698=ORIENTED_EDGE ( 'NONE', *, *, #26508, .F. ) ;
#233752=ORIENTED_EDGE ( 'NONE', *, *, #134058, .F. ) ;
#233767=CARTESIAN_POINT ( 'NONE',  ( -16.80621392010911563, 63.08289460196063203, -213.1678741730786157 ) ) ;
#233839=EDGE_CURVE ( 'NONE', #155667, #180612, #214810, .T. ) ;
#234318=EDGE_LOOP ( 'NONE', ( #187236, #182338, #67229, #187381 ) ) ;
#234475=CARTESIAN_POINT ( 'NONE',  ( 20.04999999999999716, 61.20755944685602401, -224.6372899806900989 ) ) ;
#234501=CARTESIAN_POINT ( 'NONE',  ( -17.04295772865349079, 60.86706971703560498, -221.0221225864443113 ) ) ;
#234610=AXIS2_PLACEMENT_3D ( 'NONE', #158420, #59233, #138777 ) ;
#234978=ORIENTED_EDGE ( 'NONE', *, *, #179441, .T. ) ;
#235047=CARTESIAN_POINT ( 'NONE',  ( -16.82055514392382634, 63.07871787671091823, -213.1534853438195398 ) ) ;
#235094=CARTESIAN_POINT ( 'NONE',  ( -16.92507428761699728, 60.95595224120684463, -220.9805406349763075 ) ) ;
#235147=CARTESIAN_POINT ( 'NONE',  ( 13.99999999999999822, 62.10905854918434699, -217.1108499610991203 ) ) ;
#235184=ORIENTED_EDGE ( 'NONE', *, *, #108970, .F. ) ;
#235563=CARTESIAN_POINT ( 'NONE',  ( -16.94389599338511943, 60.88850954836924245, -221.0718225180464174 ) ) ;
#235586=CARTESIAN_POINT ( 'NONE',  ( -18.38204789744325396, 62.49951772298229713, -209.4458114573654655 ) ) ;
#235631=CARTESIAN_POINT ( 'NONE',  ( -16.94107738177415712, 60.85118289042637940, -221.1214263997032106 ) ) ;
#235854=CARTESIAN_POINT ( 'NONE',  ( -18.34374000495060386, 58.57934086597919077, -223.9244941873113817 ) ) ;
#236091=CARTESIAN_POINT ( 'NONE',  ( -16.87036670365548474, 63.08160062417908165, -212.9922606024214531 ) ) ;
#236183=CARTESIAN_POINT ( 'NONE',  ( -17.11825945287482753, 60.86901957628278836, -220.9190389461266477 ) ) ;
#236315=CARTESIAN_POINT ( 'NONE',  ( -16.97683810757273193, 62.92512680882908427, -213.7198058836067389 ) ) ;
#236523=DIRECTION ( 'NONE',  ( 0.7071067811865456854, 0.6824534298470390503, -0.1850873201762214815 ) ) ;
#236588=CARTESIAN_POINT ( 'NONE',  ( -16.90987985657661241, 63.08324549817244531, -213.1069633031077615 ) ) ;
#236591=EDGE_LOOP ( 'NONE', ( #19599, #169805, #200653, #62634 ) ) ;
#236710=CARTESIAN_POINT ( 'NONE',  ( -16.86445178670630440, 60.91689827996518147, -221.0778870335527415 ) ) ;
#236833=EDGE_CURVE ( 'NONE', #110195, #66925, #239407, .T. ) ;
#236891=VERTEX_POINT ( 'NONE', #106878 ) ;
#237053=DIRECTION ( 'NONE',  ( -1.000000000000000000, 0.000000000000000000, 0.000000000000000000 ) ) ;
#237081=ORIENTED_EDGE ( 'NONE', *, *, #157075, .F. ) ;
#237248=EDGE_CURVE ( 'NONE', #230787, #253697, #139176, .T. ) ;
#237500=EDGE_LOOP ( 'NONE', ( #113553, #82627, #29730, #147232, #65205 ) ) ;
#237630=ORIENTED_EDGE ( 'NONE', *, *, #57388, .T. ) ;
#237799=EDGE_LOOP ( 'NONE', ( #253615, #203002, #241921 ) ) ;
#237838=VERTEX_POINT ( 'NONE', #129683 ) ;
#237844=DIRECTION ( 'NONE',  ( 1.000000000000000000, 0.000000000000000000, 0.000000000000000000 ) ) ;
#237882=CARTESIAN_POINT ( 'NONE',  ( -17.73285935860488038, 62.83985570472179205, -210.5653675750546086 ) ) ;
#237918=CARTESIAN_POINT ( 'NONE',  ( -21.65000000000000213, 65.69159657275406516, -213.8343546826533839 ) ) ;
#238172=CARTESIAN_POINT ( 'NONE',  ( 20.05000000000002913, 62.65526179112260508, -225.0299194783148664 ) ) ;
#238228=CARTESIAN_POINT ( 'NONE',  ( -16.91256925476570316, 63.08204023972218266, -213.0047279777396625 ) ) ;
#238354=ORIENTED_EDGE ( 'NONE', *, *, #190262, .F. ) ;
#238512=VERTEX_POINT ( 'NONE', #255831 ) ;
#238644=ORIENTED_EDGE ( 'NONE', *, *, #206821, .F. ) ;
#238675=DIRECTION ( 'NONE',  ( -1.073024830501117725E-15, 0.2617529984165031243, 0.9651348961777157509 ) ) ;
#238676=ORIENTED_EDGE ( 'NONE', *, *, #188872, .T. ) ;
#238798=CARTESIAN_POINT ( 'NONE',  ( -16.97683809663754317, 62.92304522977585890, -213.7274810758511592 ) ) ;
#238830=DIRECTION ( 'NONE',  ( 0.000000000000000000, 0.2617529984165031243, 0.9651348961777157509 ) ) ;
#238947=CARTESIAN_POINT ( 'NONE',  ( 12.25000000000000178, 62.53182050776835865, -217.4622410876596064 ) ) ;
#238969=CARTESIAN_POINT ( 'NONE',  ( -33.72168855820452649, 62.50563584222673796, -209.4474707446456421 ) ) ;
#238993=DIRECTION ( 'NONE',  ( 0.000000000000000000, -0.2617529984165031243, -0.9651348961777157509 ) ) ;
#239399=CARTESIAN_POINT ( 'NONE',  ( -16.77683809663752257, 63.08610022504904435, -213.1421742787362064 ) ) ;
#239407=CIRCLE ( 'NONE', #51938, 1.749999999999999778 ) ;
#239504=CARTESIAN_POINT ( 'NONE',  ( -16.94309007106720344, 60.88703202972964590, -221.0733422789901113 ) ) ;
#239509=CARTESIAN_POINT ( 'NONE',  ( 20.99999999999999645, 63.27875933230978234, -213.1799721866121047 ) ) ;
#239632=CARTESIAN_POINT ( 'NONE',  ( 17.23472005113827166, 60.28074582209914212, -222.1029091445273593 ) ) ;
#239798=EDGE_LOOP ( 'NONE', ( #21436, #222741, #152959, #250574 ) ) ;
#240095=ORIENTED_EDGE ( 'NONE', *, *, #160438, .F. ) ;
#240208=CARTESIAN_POINT ( 'NONE',  ( -18.40000000000000213, 67.23581240663841641, -214.2531594801197627 ) ) ;
#240238=CARTESIAN_POINT ( 'NONE',  ( 13.22261339317536866, 62.09660346237240702, -218.7363060264990509 ) ) ;
#240255=LINE ( 'NONE', #238969, #60791 ) ;
#240350=ORIENTED_EDGE ( 'NONE', *, *, #183969, .T. ) ;
#240443=VERTEX_POINT ( 'NONE', #101306 ) ;
#240453=CARTESIAN_POINT ( 'NONE',  ( -16.94107738177414291, 63.04990807712501777, -213.0142932718104021 ) ) ;
#240611=EDGE_LOOP ( 'NONE', ( #23587, #98146 ) ) ;
#240667=LINE ( 'NONE', #137692, #14127 ) ;
#240811=CARTESIAN_POINT ( 'NONE',  ( -16.94107738177414291, 63.04990807712501777, -213.0142932718103737 ) ) ;
#240931=CARTESIAN_POINT ( 'NONE',  ( 18.39999999999999503, 65.08943781962308606, -222.1672656287770451 ) ) ;
#241187=DIRECTION ( 'NONE',  ( 0.000000000000000000, -0.9651348961777157509, 0.2617529984165031243 ) ) ;
#241193=VECTOR ( 'NONE', #59747, 1000.000000000000000 ) ;
#241384=ORIENTED_EDGE ( 'NONE', *, *, #33245, .F. ) ;
#241506=CARTESIAN_POINT ( 'NONE',  ( 14.45204356427543146, 62.05093865251256346, -218.8507522889722168 ) ) ;
#241520=LINE ( 'NONE', #242792, #193813 ) ;
#241537=EDGE_CURVE ( 'NONE', #180046, #90818, #70334, .T. ) ;
#241584=EDGE_CURVE ( 'NONE', #186519, #10339, #119911, .T. ) ;
#241628=ORIENTED_EDGE ( 'NONE', *, *, #255740, .F. ) ;
#241734=CARTESIAN_POINT ( 'NONE',  ( -18.44085059012131822, 62.46367190038257178, -209.4461346550174312 ) ) ;
#241772=CARTESIAN_POINT ( 'NONE',  ( -16.95709691156337229, 63.08309975593071783, -213.1373284914761825 ) ) ;
#241909=DIRECTION ( 'NONE',  ( 1.186688945009010077E-16, 0.9651348961777157509, -0.2617529984165031243 ) ) ;
#241921=ORIENTED_EDGE ( 'NONE', *, *, #105959, .F. ) ;
#241958=CARTESIAN_POINT ( 'NONE',  ( -16.88495309932520883, 60.93084759950085783, -221.0554292032533112 ) ) ;
#242020=( NAMED_UNIT ( * ) PLANE_ANGLE_UNIT ( ) SI_UNIT ( $, .RADIAN. ) );
#242032=( BOUNDED_SURFACE ( )  B_SPLINE_SURFACE ( 3, 2, ( 
 ( #42299, #124413, #166136 ),
 ( #201365, #241772, #1858 ),
 ( #245636, #24039, #102225 ),
 ( #140089, #160976, #145233 ) ),
 .UNSPECIFIED., .F., .F., .F. ) 
 B_SPLINE_SURFACE_WITH_KNOTS ( ( 4, 4 ),
 ( 3, 3 ),
 ( 3.658908243880901523, 4.712388980384689674 ),
 ( 0.000000000000000000, 1.000000000000000000 ),
 .UNSPECIFIED. ) 
 GEOMETRIC_REPRESENTATION_ITEM ( )  RATIONAL_B_SPLINE_SURFACE ( (
 ( 1.000000000000000000, 0.8984936768950856356, 1.000000000000000000),
 ( 1.000000000000000000, 0.8646876308616651130, 1.000000000000000000),
 ( 1.000000000000000000, 0.7953136715911847121, 1.000000000000000000),
 ( 1.000000000000000000, 0.7071067811866510455, 1.000000000000000000) ) ) 
 REPRESENTATION_ITEM ( '' )  SURFACE ( )  );
#242165=CARTESIAN_POINT ( 'NONE',  ( -16.84981964351505113, 61.02838145972558692, -220.8383371048568904 ) ) ;
#242258=CARTESIAN_POINT ( 'NONE',  ( -18.34374000495059676, 62.50563584222673796, -209.4474707446456421 ) ) ;
#242294=CARTESIAN_POINT ( 'NONE',  ( -16.89060415895971090, 60.93711167174846111, -221.0453457311873819 ) ) ;
#242391=VECTOR ( 'NONE', #243681, 1000.000000000000000 ) ;
#242434=DIRECTION ( 'NONE',  ( -0.000000000000000000, 0.2617529984165031243, 0.9651348961777157509 ) ) ;
#242518=DIRECTION ( 'NONE',  ( -0.000000000000000000, 0.2617529984165031243, 0.9651348961777157509 ) ) ;
#242575=VECTOR ( 'NONE', #175660, 1000.000000000000000 ) ;
#242792=CARTESIAN_POINT ( 'NONE',  ( 20.27550659511088682, 61.64772458173430181, -221.2338429919259966 ) ) ;
#242911=VERTEX_POINT ( 'NONE', #197869 ) ;
#242974=CARTESIAN_POINT ( 'NONE',  ( -16.93353400591626112, 63.05466693176257564, -213.0335249609126151 ) ) ;
#243092=ADVANCED_FACE ( 'NONE', ( #128618 ), #167764, .F. ) ;
#243144=VERTEX_POINT ( 'NONE', #68645 ) ;
#243295=FILL_AREA_STYLE ('',( #180778 ) ) ;
#243681=DIRECTION ( 'NONE',  ( 1.652117596168391700E-15, -0.9651348961777157509, 0.2617529984165031243 ) ) ;
#244033=FACE_OUTER_BOUND ( 'NONE', #98225, .T. ) ;
#244102=DIRECTION ( 'NONE',  ( 0.000000000000000000, 0.2617529984165026802, 0.9651348961777159730 ) ) ;
#244129=CARTESIAN_POINT ( 'NONE',  ( -16.97683809663752186, 62.88879881541066652, -213.8537543555185607 ) ) ;
#244628=CARTESIAN_POINT ( 'NONE',  ( -16.87331047859649757, 63.08573235307424198, -213.1276215869287967 ) ) ;
#244647=AXIS2_PLACEMENT_3D ( 'NONE', #177297, #57291, #37775 ) ;
#244740=ORIENTED_EDGE ( 'NONE', *, *, #63063, .T. ) ;
#244801=CARTESIAN_POINT ( 'NONE',  ( -12.68215100488890457, 62.84948463577724453, -216.1128043527995430 ) ) ;
#245049=ORIENTED_EDGE ( 'NONE', *, *, #76715, .F. ) ;
#245172=ORIENTED_EDGE ( 'NONE', *, *, #159796, .T. ) ;
#245475=B_SPLINE_CURVE_WITH_KNOTS ( 'NONE', 3,
 ( #182347, #242294, #104050, #80639, #143190, #63660, #44108, #40293, #123653, #68484 ),
 .UNSPECIFIED., .F., .F.,
 ( 4, 3, 3, 4 ),
 ( 1.961400829040844664E-15, 8.145022132830484647E-06, 1.905645951092394214E-05, 2.061107371225745169E-05 ),
 .UNSPECIFIED. ) ;
#245499=CARTESIAN_POINT ( 'NONE',  ( -18.40000000000000213, 59.44312576075365229, -220.7395490299249445 ) ) ;
#245636=CARTESIAN_POINT ( 'NONE',  ( -17.01764560440378204, 63.05955705343778561, -213.2241350757899454 ) ) ;
#245860=CYLINDRICAL_SURFACE ( 'NONE', #208136, 0.1000000000000106498 ) ;
#246259=CARTESIAN_POINT ( 'NONE',  ( 21.13736287352038445, 62.77635462851659298, -221.5399373006264625 ) ) ;
#246324=CARTESIAN_POINT ( 'NONE',  ( -16.87036670365549895, 60.78293754744167643, -221.1029176676855741 ) ) ;
#246594=CARTESIAN_POINT ( 'NONE',  ( -23.25000000000000355, 60.04939757144280321, -224.3231863825903076 ) ) ;
#246678=CARTESIAN_POINT ( 'NONE',  ( -17.04761207306819770, 60.86557236029944562, -221.0217164902426248 ) ) ;
#246696=EDGE_LOOP ( 'NONE', ( #72162, #215037, #97392 ) ) ;
#246880=CARTESIAN_POINT ( 'NONE',  ( 16.87683809663750267, 60.93935776605891164, -221.0417277355860790 ) ) ;
#246955=FACE_OUTER_BOUND ( 'NONE', #234318, .T. ) ;
#247160=FACE_OUTER_BOUND ( 'NONE', #5956, .T. ) ;
#247263=AXIS2_PLACEMENT_3D ( 'NONE', #227699, #25669, #89471 ) ;
#247276=CARTESIAN_POINT ( 'NONE',  ( 18.39999999999999503, 67.23581240663841641, -214.2531594801197627 ) ) ;
#247311=ORIENTED_EDGE ( 'NONE', *, *, #93281, .F. ) ;
#247525=VECTOR ( 'NONE', #18099, 1000.000000000000000 ) ;
#247533=CARTESIAN_POINT ( 'NONE',  ( 20.09999999999999787, 60.24242455067834356, -224.3755369822736156 ) ) ;
#247539=( NAMED_UNIT ( * ) SI_UNIT ( $, .STERADIAN. ) SOLID_ANGLE_UNIT ( ) );
#247694=LINE ( 'NONE', #187743, #76532 ) ;
#247895=ORIENTED_EDGE ( 'NONE', *, *, #17385, .F. ) ;
#248062=AXIS2_PLACEMENT_3D ( 'NONE', #68338, #108741, #227397 ) ;
#248128=EDGE_CURVE ( 'NONE', #249995, #91602, #133708, .T. ) ;
#248385=CARTESIAN_POINT ( 'NONE',  ( -17.73285935862742235, 59.43258456655187416, -223.1286478281496954 ) ) ;
#248663=CARTESIAN_POINT ( 'NONE',  ( -12.60829076262180592, 62.83279349218706500, -216.2014764372737829 ) ) ;
#248940=CARTESIAN_POINT ( 'NONE',  ( -16.81744102076749314, 60.93935776605891164, -221.0417277355860790 ) ) ;
#249009=ORIENTED_EDGE ( 'NONE', *, *, #206821, .T. ) ;
#249183=CARTESIAN_POINT ( 'NONE',  ( 12.48201962039796520, 62.79576509294746955, -216.3871738676108691 ) ) ;
#249196=EDGE_CURVE ( 'NONE', #7786, #211757, #168647, .T. ) ;
#249336=LINE ( 'NONE', #229754, #241193 ) ;
#249703=CARTESIAN_POINT ( 'NONE',  ( -16.77683809663752257, 48.78215419113038109, -213.4964773079645681 ) ) ;
#249809=CARTESIAN_POINT ( 'NONE',  ( -17.78043020864321733, 62.81909162847866668, -210.6586991758544798 ) ) ;
#249995=VERTEX_POINT ( 'NONE', #164530 ) ;
#250103=CARTESIAN_POINT ( 'NONE',  ( -16.87036670365548474, 62.98166273414030059, -212.9957845397927656 ) ) ;
#250117=CARTESIAN_POINT ( 'NONE',  ( -23.25000000000000355, 58.31215475832291162, -223.8520309854405923 ) ) ;
#250361=CARTESIAN_POINT ( 'NONE',  ( -16.77732147278574715, 60.94678617778803442, -221.0297456304129753 ) ) ;
#250534=CARTESIAN_POINT ( 'NONE',  ( -17.78043020864319956, 59.46182193223923207, -223.0376142573344111 ) ) ;
#250567=LINE ( 'NONE', #193191, #121290 ) ;
#250574=ORIENTED_EDGE ( 'NONE', *, *, #98781, .T. ) ;
#250687=CARTESIAN_POINT ( 'NONE',  ( 12.25000000000000000, 62.59162599727320497, -217.2417264603073761 ) ) ;
#250736=VERTEX_POINT ( 'NONE', #98739 ) ;
#250881=DIRECTION ( 'NONE',  ( 0.000000000000000000, -0.9651348961777157509, 0.2617529984165031243 ) ) ;
#250949=CARTESIAN_POINT ( 'NONE',  ( -16.89208623190940628, 63.08558943445424916, -213.1221201667474361 ) ) ;
#251194=ORIENTED_EDGE ( 'NONE', *, *, #225353, .F. ) ;
#251228=DIRECTION ( 'NONE',  ( -0.000000000000000000, 0.2617529984165031243, 0.9651348961777157509 ) ) ;
#251276=CARTESIAN_POINT ( 'NONE',  ( -18.40000000000000213, 62.49259288703249382, -209.4955626911903721 ) ) ;
#251297=CARTESIAN_POINT ( 'NONE',  ( -18.39418127959864435, 62.49526672404898164, -209.4446585493922157 ) ) ;
#251819=CARTESIAN_POINT ( 'NONE',  ( -17.29158576265543346, 60.21639215357974706, -222.1229442910193370 ) ) ;
#251852=DIRECTION ( 'NONE',  ( 1.186688945009010077E-16, 0.9651348961777157509, -0.2617529984165031243 ) ) ;
#251865=ADVANCED_FACE ( 'NONE', ( #15458 ), #217467, .T. ) ;
#251908=LINE ( 'NONE', #148983, #108855 ) ;
#251941=CARTESIAN_POINT ( 'NONE',  ( 18.54999999999999716, 61.20755944685601690, -224.6372899806900989 ) ) ;
#252240=CARTESIAN_POINT ( 'NONE',  ( -16.89146115310545682, 63.08560170894831032, -213.1225895282340730 ) ) ;
#252400=ORIENTED_EDGE ( 'NONE', *, *, #125672, .T. ) ;
#252585=CARTESIAN_POINT ( 'NONE',  ( 18.54999999999999716, 61.20755944685601690, -224.6372899806900989 ) ) ;
#252864=ORIENTED_EDGE ( 'NONE', *, *, #13309, .T. ) ;
#252944=EDGE_CURVE ( 'NONE', #253697, #5980, #113479, .T. ) ;
#252994=CIRCLE ( 'NONE', #44898, 0.9000000000000014655 ) ;
#253038=EDGE_CURVE ( 'NONE', #151077, #242911, #47117, .T. ) ;
#253300=B_SPLINE_CURVE_WITH_KNOTS ( 'NONE', 3,
 ( #62828, #204890, #146204, #184054, #225727, #105776, #5390, #186644, #84921, #164512, #47092, #65393, #144914, #101925, #126653, #8005, #82357, #142357, #11870, #191795, #9272, #112245, #133081, #249183, #70566, #169680, #212624, #10571, #151375, #148797 ),
 .UNSPECIFIED., .F., .F.,
 ( 4, 2, 2, 2, 2, 2, 2, 2, 2, 2, 2, 2, 2, 2, 4 ),
 ( 0.000000000000000000, 0.0003422764154113342653, 0.0006845528308226685307, 0.001026829246234002742, 0.001369105661645337061, 0.002053658492468007218, 0.002738211323290677159, 0.003080487738702009527, 0.003422764154113341895, 0.003765040569524674696, 0.004107316984936006631, 0.004449593400347339432, 0.004791869815758671367, 0.005134146231170004168, 0.005476422646581336103 ),
 .UNSPECIFIED. ) ;
#253411=CARTESIAN_POINT ( 'NONE',  ( -21.64999999999999858, 60.86901957628278836, -220.9190389461266477 ) ) ;
#253414=DIRECTION ( 'NONE',  ( 1.186688945009009831E-16, 0.9651348961777157509, -0.2617529984165031243 ) ) ;
#253615=ORIENTED_EDGE ( 'NONE', *, *, #252944, .T. ) ;
#253697=VERTEX_POINT ( 'NONE', #245499 ) ;
#253794=LINE ( 'NONE', #171741, #97072 ) ;
#254320=DIRECTION ( 'NONE',  ( 1.000000000000000000, 0.000000000000000000, 0.000000000000000000 ) ) ;
#254468=CARTESIAN_POINT ( 'NONE',  ( -16.86133551771150607, 63.07299635117417580, -213.1745817361760089 ) ) ;
#254575=AXIS2_PLACEMENT_3D ( 'NONE', #129001, #53308, #169444 ) ;
#254602=ORIENTED_EDGE ( 'NONE', *, *, #148210, .T. ) ;
#254698=EDGE_CURVE ( 'NONE', #116061, #158643, #39653, .T. ) ;
#254719=CARTESIAN_POINT ( 'NONE',  ( -20.65000000000000568, 65.69159657275406516, -213.8343546826533839 ) ) ;
#254942=CARTESIAN_POINT ( 'NONE',  ( -16.91256925476571737, 60.87407910423024049, -221.1459158692213691 ) ) ;
#255080=CARTESIAN_POINT ( 'NONE',  ( -18.40000000000000213, 62.49259387941005173, -209.4439336506227960 ) ) ;
#255110=EDGE_LOOP ( 'NONE', ( #120, #129977, #152269, #113058 ) ) ;
#255148=CARTESIAN_POINT ( 'NONE',  ( -16.93658211146646408, 60.88257505944956449, -221.0825842276667856 ) ) ;
#255740=EDGE_CURVE ( 'NONE', #20388, #99952, #116959, .T. ) ;
#255750=ORIENTED_EDGE ( 'NONE', *, *, #116568, .T. ) ;
#255824=ORIENTED_EDGE ( 'NONE', *, *, #14568, .T. ) ;
#255831=CARTESIAN_POINT ( 'NONE',  ( 18.39999999999997371, 62.50563584222673796, -209.4474707446456421 ) ) ;
#255833=CARTESIAN_POINT ( 'NONE',  ( -16.82542659449979539, 63.07592089668835911, -213.2230149068291212 ) ) ;
#256056=DIRECTION ( 'NONE',  ( 1.000000000000000000, -1.145314911736513911E-16, 3.106193895438251633E-17 ) ) ;
#256112=CARTESIAN_POINT ( 'NONE',  ( -15.75000000000000355, 62.10905854918435409, -217.1108499610990918 ) ) ;
#256216=FACE_OUTER_BOUND ( 'NONE', #106978, .T. ) ;
#256220=EDGE_LOOP ( 'NONE', ( #82889, #207313, #142958, #217783 ) ) ;
#256376=EDGE_LOOP ( 'NONE', ( #45955, #233752, #117835, #214759 ) ) ;
#256526=UNCERTAINTY_MEASURE_WITH_UNIT (LENGTH_MEASURE( 1.000000000000000082E-05 ), #102480, 'distance_accuracy_value', 'NONE');
#256578=EDGE_CURVE ( 'NONE', #70322, #50778, #247694, .T. ) ;
#256651=LINE ( 'NONE', #165313, #124776 ) ;
#256863=DIRECTION ( 'NONE',  ( -1.186688945009010077E-16, -0.9651348961777157509, 0.2617529984165031243 ) ) ;
#257018=CARTESIAN_POINT ( 'NONE',  ( -16.89021194854741026, 63.05761173939616526, -213.2313078320790396 ) ) ;
#257322=CARTESIAN_POINT ( 'NONE',  ( -15.55912972643740488, 64.49398937010923305, -213.5095531679024532 ) ) ;
#257387=CARTESIAN_POINT ( 'NONE',  ( -16.94333152882356686, 63.05779874932826345, -213.0764958470617785 ) ) ;
#257712=CARTESIAN_POINT ( 'NONE',  ( -16.94037747912386394, 60.85215442253927165, -221.1205180743122298 ) ) ;
#257873=EDGE_LOOP ( 'NONE', ( #76737, #52615, #146035, #169915 ) ) ;
#257876=VERTEX_POINT ( 'NONE', #35149 ) ;
#258099=CARTESIAN_POINT ( 'NONE',  ( 23.24999999999999645, 58.31215475832291162, -223.8520309854405923 ) ) ;
ENDSEC;
END-ISO-10303-21;
